ISO-10303-21;
HEADER;
FILE_DESCRIPTION (('STEP AP214'),
    '1' );
FILE_NAME ('hex flange nut gradea_iso_ISO - 4161 - M6 - N.step',
    '2026-09-24T10:26:00',
    ( '' ),
    ( '' ),
    'SwSTEP 2.0',
    'SolidWorks 2026',
    '' );
FILE_SCHEMA (( 'AUTOMOTIVE_DESIGN' ));
ENDSEC;

DATA;
#14=AXIS2_PLACEMENT_3D ( 'NONE', #9418, #3869, #11768 ) ;
#32=VERTEX_POINT ( 'NONE', #2048 ) ;
#38=CARTESIAN_POINT ( 'NONE',  ( 3.903127820947815962E-15, 5.773502691896270633, -0.5999999999999894307 ) ) ;
#62=CIRCLE ( 'NONE', #4962, 5.000000000000000888 ) ;
#64=CARTESIAN_POINT ( 'NONE',  ( 0.000000000000000000, 0.000000000000000000, 0.000000000000000000 ) ) ;
#83=CARTESIAN_POINT ( 'NONE',  ( -5.000000000000000000, 0.9888715124523217437, -0.07061148569344526116 ) ) ;
#84=CARTESIAN_POINT ( 'NONE',  ( -5.244935917792783897, 2.071347852254889155, -4.480280589322315876 ) ) ;
#89=LINE ( 'NONE', #9889, #12206 ) ;
#137=CARTESIAN_POINT ( 'NONE',  ( 3.000000000000000888, 3.469446951953614189E-15, -25.03750572909319061 ) ) ;
#148=CARTESIAN_POINT ( 'NONE',  ( 0.8653900595644522520, -5.556556492855608376, -4.490801088233122407 ) ) ;
#155=ORIENTED_EDGE ( 'NONE', *, *, #6137, .F. ) ;
#167=CARTESIAN_POINT ( 'NONE',  ( 0.000000000000000000, 0.000000000000000000, 0.000000000000000000 ) ) ;
#173=FACE_OUTER_BOUND ( 'NONE', #6648, .T. ) ;
#206=EDGE_CURVE ( 'NONE', #7155, #8446, #11531, .T. ) ;
#232=B_SPLINE_CURVE_WITH_KNOTS ( 'NONE', 3,
 ( #9885, #3384, #13193, #4342, #3307, #6720, #12149, #7750, #12227, #4273 ),
 .UNSPECIFIED., .F., .F.,
 ( 4, 2, 2, 2, 4 ),
 ( 0.000000000000000000, 0.001528561485809837566, 0.003057122971619675132, 0.004585684457429512265, 0.006114245943239350264 ),
 .UNSPECIFIED. ) ;
#240=CARTESIAN_POINT ( 'NONE',  ( -5.184911785341042467, -2.993510214990505514, -4.630720594357042863 ) ) ;
#248=CIRCLE ( 'NONE', #2365, 2.500000000000000444 ) ;
#270=DIRECTION ( 'NONE',  ( 0.000000000000000000, -8.482162385747133845E-47, 1.000000000000000000 ) ) ;
#274=CARTESIAN_POINT ( 'NONE',  ( 5.253687138749954855, 3.069401043531180484, -4.666239469495483405 ) ) ;
#278=VECTOR ( 'NONE', #5827, 1000.000000000000227 ) ;
#282=CARTESIAN_POINT ( 'NONE',  ( 5.000000000000001776, -0.9835753746177059442, -0.05800540215398873600 ) ) ;
#289=ORIENTED_EDGE ( 'NONE', *, *, #2632, .T. ) ;
#309=CARTESIAN_POINT ( 'NONE',  ( -4.177163563997808592E-15, -5.914770570062451327, -4.581776566113613391 ) ) ;
#326=CARTESIAN_POINT ( 'NONE',  ( 5.211749180171795892, 2.764497899775253398, -4.327903350935040194 ) ) ;
#331=AXIS2_PLACEMENT_3D ( 'NONE', #13223, #14112, #7625 ) ;
#364=CARTESIAN_POINT ( 'NONE',  ( 5.122341571230623281, 2.957385285031203459, -4.581776566113601845 ) ) ;
#372=DIRECTION ( 'NONE',  ( -1.000000000000000000, 0.000000000000000000, 0.000000000000000000 ) ) ;
#384=EDGE_LOOP ( 'NONE', ( #8379, #6792, #7299, #1071, #1051 ) ) ;
#394=CARTESIAN_POINT ( 'NONE',  ( -5.244818697407745312, 2.029379090245553741, -4.490884354499010023 ) ) ;
#446=LINE ( 'NONE', #6057, #278 ) ;
#460=CARTESIAN_POINT ( 'NONE',  ( 3.514986608502051801, -4.017641317387857569, -4.357689166958506277 ) ) ;
#462=ORIENTED_EDGE ( 'NONE', *, *, #8769, .F. ) ;
#472=CARTESIAN_POINT ( 'NONE',  ( 0.7030283904629636149, 5.367609061414830407, -4.396693167833897853 ) ) ;
#499=EDGE_CURVE ( 'NONE', #10194, #2629, #8920, .T. ) ;
#519=CARTESIAN_POINT ( 'NONE',  ( 2.500000000000018652, 4.330127018922186544, 0.000000000000000000 ) ) ;
#540=AXIS2_PLACEMENT_3D ( 'NONE', #6567, #938, #12142 ) ;
#546=CARTESIAN_POINT ( 'NONE',  ( 0.8333333333333354798, 5.292377467571581562, -4.118275046351174140 ) ) ;
#550=CARTESIAN_POINT ( 'NONE',  ( 4.319324222800557500, 3.279739689145082959, -4.138711833383065475 ) ) ;
#559=CARTESIAN_POINT ( 'NONE',  ( 1.432312439535594395, 4.946556719366753896, -0.1121614189353446478 ) ) ;
#567=ORIENTED_EDGE ( 'NONE', *, *, #1776, .F. ) ;
#573=LINE ( 'NONE', #10585, #7006 ) ;
#580=EDGE_CURVE ( 'NONE', #10243, #2320, #2923, .T. ) ;
#583=CARTESIAN_POINT ( 'NONE',  ( -0.8082922630888625948, -5.306834936218045584, -0.2701150775514032376 ) ) ;
#601=EDGE_CURVE ( 'NONE', #11659, #3422, #11541, .T. ) ;
#632=B_SPLINE_CURVE_WITH_KNOTS ( 'NONE', 3,
 ( #2328, #11388, #8022, #3652, #12358, #8979 ),
 .UNSPECIFIED., .F., .F.,
 ( 4, 2, 4 ),
 ( 0.002950759650825622842, 0.004429055062152257617, 0.005907350473478891958 ),
 .UNSPECIFIED. ) ;
#641=VERTEX_POINT ( 'NONE', #6850 ) ;
#686=CARTESIAN_POINT ( 'NONE',  ( -3.401922400370679167, -3.809401878279965015, -4.271474537230584900 ) ) ;
#693=CARTESIAN_POINT ( 'NONE',  ( -5.236872748402765509, -8.016972670139777574E-14, -4.357689166958463645 ) ) ;
#711=EDGE_LOOP ( 'NONE', ( #8770, #6169 ) ) ;
#724=ORIENTED_EDGE ( 'NONE', *, *, #11650, .F. ) ;
#735=CARTESIAN_POINT ( 'NONE',  ( 3.903127820947815962E-15, 5.773502691896270633, -0.5999999999999894307 ) ) ;
#772=CARTESIAN_POINT ( 'NONE',  ( 2.500000000000018652, 4.330127018922186544, 0.000000000000000000 ) ) ;
#783=CARTESIAN_POINT ( 'NONE',  ( -0.4317663827706254565, -5.811727376006682988, -4.566919140436432656 ) ) ;
#803=DIRECTION ( 'NONE',  ( 0.000000000000000000, -8.482162385747133845E-47, 1.000000000000000000 ) ) ;
#814=( LENGTH_UNIT ( ) NAMED_UNIT ( * ) SI_UNIT ( .MILLI., .METRE. ) );
#821=CARTESIAN_POINT ( 'NONE',  ( -5.000000000000004441, 2.886751345948121106, -4.369520038198754897 ) ) ;
#860=FACE_BOUND ( 'NONE', #711, .T. ) ;
#865=AXIS2_PLACEMENT_3D ( 'NONE', #12482, #2679, #8292 ) ;
#867=ADVANCED_FACE ( 'NONE', ( #6458 ), #6254, .F. ) ;
#881=DIRECTION ( 'NONE',  ( 0.000000000000000000, 8.482162385747133845E-47, -1.000000000000000000 ) ) ;
#920=ORIENTED_EDGE ( 'NONE', *, *, #12804, .T. ) ;
#928=EDGE_CURVE ( 'NONE', #2320, #12268, #10145, .T. ) ;
#938=DIRECTION ( 'NONE',  ( 0.000000000000000000, -8.482162385747133845E-47, 1.000000000000000000 ) ) ;
#949=( NAMED_UNIT ( * ) SI_UNIT ( $, .STERADIAN. ) SOLID_ANGLE_UNIT ( ) );
#981=VERTEX_POINT ( 'NONE', #3344 ) ;
#990=CARTESIAN_POINT ( 'NONE',  ( -4.400655246570065238, 3.515428273946862081, -4.476900509771544634 ) ) ;
#995=ADVANCED_FACE ( 'NONE', ( #173 ), #1332, .T. ) ;
#1019=EDGE_LOOP ( 'NONE', ( #1037, #10562, #14464, #7799, #6389 ) ) ;
#1022=EDGE_LOOP ( 'NONE', ( #14207, #7938, #8866, #13147 ) ) ;
#1025=( NAMED_UNIT ( * ) PLANE_ANGLE_UNIT ( ) SI_UNIT ( $, .RADIAN. ) );
#1034=( BOUNDED_SURFACE ( )  B_SPLINE_SURFACE ( 3, 2, ( 
 ( #326, #10490, #10644 ),
 ( #550, #8212, #9546 ),
 ( #11660, #8440, #9242 ),
 ( #6084, #5072, #4855 ),
 ( #7037, #472, #12680 ),
 ( #10566, #4789, #6964 ) ),
 .UNSPECIFIED., .F., .F., .F. ) 
 B_SPLINE_SURFACE_WITH_KNOTS ( ( 4, 2, 4 ),
 ( 3, 3 ),
 ( 0.002450104044831662945, 0.005591829551853648266, 0.008733555058875634020 ),
 ( 0.000000000000000000, 1.000000000000000000 ),
 .UNSPECIFIED. ) 
 GEOMETRIC_REPRESENTATION_ITEM ( )  RATIONAL_B_SPLINE_SURFACE ( (
 ( 1.000000000000000000, 0.8047731410850403888, 1.000000000000000000),
 ( 1.000000000000000000, 0.8125552299158879110, 1.000000000000000000),
 ( 1.000000000000000000, 0.8191520442886336406, 1.000000000000000000),
 ( 1.000000000000000000, 0.8191520442893395204, 1.000000000000000000),
 ( 1.000000000000000000, 0.8125552299153580016, 1.000000000000000000),
 ( 1.000000000000000000, 0.8047731410850398337, 1.000000000000000000) ) ) 
 REPRESENTATION_ITEM ( '' )  SURFACE ( )  );
#1037=ORIENTED_EDGE ( 'NONE', *, *, #9678, .F. ) ;
#1051=ORIENTED_EDGE ( 'NONE', *, *, #10353, .T. ) ;
#1068=CARTESIAN_POINT ( 'NONE',  ( -2.500000000000011990, 4.330127018922186544, 0.000000000000000000 ) ) ;
#1071=ORIENTED_EDGE ( 'NONE', *, *, #8262, .T. ) ;
#1080=CARTESIAN_POINT ( 'NONE',  ( -3.081487911019577365E-30, 3.469446951953614189E-15, -4.900000000000015454 ) ) ;
#1086=ADVANCED_FACE ( 'NONE', ( #2584 ), #10635, .T. ) ;
#1092=FILL_AREA_STYLE ('',( #12226 ) ) ;
#1102=DIRECTION ( 'NONE',  ( 1.000000000000000000, 0.000000000000000000, 0.000000000000000000 ) ) ;
#1128=VERTEX_POINT ( 'NONE', #12675 ) ;
#1137=DIRECTION ( 'NONE',  ( 0.8191520442889909104, 1.003171929053523637E-16, -0.5735764363510472696 ) ) ;
#1146=ORIENTED_EDGE ( 'NONE', *, *, #4200, .T. ) ;
#1166=CARTESIAN_POINT ( 'NONE',  ( -5.000000000000000888, 2.092595045405802434, -4.400086043326545848 ) ) ;
#1230=DIRECTION ( 'NONE',  ( 0.9396926207859143121, 1.150791560227857665E-16, -0.3420201433256522816 ) ) ;
#1236=EDGE_CURVE ( 'NONE', #14260, #9831, #6440, .T. ) ;
#1254=DIRECTION ( 'NONE',  ( -0.000000000000000000, -8.482162385747133845E-47, 1.000000000000000000 ) ) ;
#1256=ORIENTED_EDGE ( 'NONE', *, *, #2632, .F. ) ;
#1288=FACE_OUTER_BOUND ( 'NONE', #7499, .T. ) ;
#1289=CARTESIAN_POINT ( 'NONE',  ( 5.253679160503864409, -3.068491175858450770, -4.666069923292693211 ) ) ;
#1299=ORIENTED_EDGE ( 'NONE', *, *, #2358, .T. ) ;
#1301=CARTESIAN_POINT ( 'NONE',  ( 5.253368672218637236, -3.033033817057797510, -4.659491423763650886 ) ) ;
#1307=EDGE_CURVE ( 'NONE', #10332, #32, #3164, .T. ) ;
#1321=ORIENTED_EDGE ( 'NONE', *, *, #3326, .F. ) ;
#1331=UNCERTAINTY_MEASURE_WITH_UNIT (LENGTH_MEASURE( 1.000000000000000082E-05 ), #10231, 'distance_accuracy_value', 'NONE');
#1332=PLANE ( 'NONE',  #12478 ) ;
#1334=AXIS2_PLACEMENT_3D ( 'NONE', #3699, #6904, #10418 ) ;
#1335=EDGE_LOOP ( 'NONE', ( #7967, #9486, #2581, #7234, #12217, #11618, #7087 ) ) ;
#1345=CARTESIAN_POINT ( 'NONE',  ( -4.999999999999999112, 1.924500897298744517, -4.118275046351175916 ) ) ;
#1355=ADVANCED_FACE ( 'NONE', ( #8074 ), #11466, .T. ) ;
#1375=CARTESIAN_POINT ( 'NONE',  ( -5.000000000000000000, 1.069517409952100095, -4.273100593733644814 ) ) ;
#1418=B_SPLINE_CURVE_WITH_KNOTS ( 'NONE', 3,
 ( #3045, #5146, #11813, #546, #6237 ),
 .UNSPECIFIED., .F., .F.,
 ( 4, 1, 4 ),
 ( 0.000000000000000000, 0.002886751345948135056, 0.005773502691896269245 ),
 .UNSPECIFIED. ) ;
#1420=CARTESIAN_POINT ( 'NONE',  ( 3.000000000000000888, 3.469446951953614189E-15, -6.000000000000005329 ) ) ;
#1434=ORIENTED_EDGE ( 'NONE', *, *, #7156, .T. ) ;
#1435=CARTESIAN_POINT ( 'NONE',  ( -5.000000000000000000, -0.4954705650270034845, 7.301424005332068923E-16 ) ) ;
#1458=CARTESIAN_POINT ( 'NONE',  ( -5.000000000000000000, 1.088034370075782409, -4.020973883015756201 ) ) ;
#1468=B_SPLINE_CURVE_WITH_KNOTS ( 'NONE', 3,
 ( #1515, #14045, #12705, #11836, #1580 ),
 .UNSPECIFIED., .F., .F.,
 ( 4, 1, 4 ),
 ( 0.000000000000000000, 0.002886751345948134623, 0.005773502691896269245 ),
 .UNSPECIFIED. ) ;
#1483=LINE ( 'NONE', #11353, #14080 ) ;
#1498=CARTESIAN_POINT ( 'NONE',  ( -5.000000000000003553, -1.924500897298772939, -4.118275046351175028 ) ) ;
#1503=FACE_OUTER_BOUND ( 'NONE', #6913, .T. ) ;
#1509=ORIENTED_EDGE ( 'NONE', *, *, #9134, .T. ) ;
#1515=CARTESIAN_POINT ( 'NONE',  ( -5.000000000000001776, -2.886751345948152192, -4.284345921091780696 ) ) ;
#1520=DIRECTION ( 'NONE',  ( 1.000000000000000000, 0.000000000000000000, 0.000000000000000000 ) ) ;
#1580=CARTESIAN_POINT ( 'NONE',  ( -1.752700365193367750E-15, -5.773502691896304384, -4.284345921091780696 ) ) ;
#1585=CARTESIAN_POINT ( 'NONE',  ( 0.000000000000000000, 0.000000000000000000, 0.000000000000000000 ) ) ;
#1604=DIRECTION ( 'NONE',  ( 0.000000000000000000, -8.482162385747133845E-47, 1.000000000000000000 ) ) ;
#1608=CARTESIAN_POINT ( 'NONE',  ( 4.379424050594069584, 3.527728022193128865, -4.490801088233107308 ) ) ;
#1625=CARTESIAN_POINT ( 'NONE',  ( -5.000000000000001776, -2.886751345948152192, -4.369520038198755785 ) ) ;
#1632=CARTESIAN_POINT ( 'NONE',  ( 5.000000000000001776, 2.886751345948127767, -6.000000000000005329 ) ) ;
#1642=ADVANCED_FACE ( 'NONE', ( #5702 ), #9843, .T. ) ;
#1663=CARTESIAN_POINT ( 'NONE',  ( 0.000000000000000000, 0.000000000000000000, 0.000000000000000000 ) ) ;
#1701=AXIS2_PLACEMENT_3D ( 'NONE', #13476, #10899, #2207 ) ;
#1712=CARTESIAN_POINT ( 'NONE',  ( 5.238704763094644612, 1.015773027556919228, -4.385839086323478853 ) ) ;
#1738=VERTEX_POINT ( 'NONE', #2953 ) ;
#1760=DIRECTION ( 'NONE',  ( 0.000000000000000000, -8.482162385747133845E-47, 1.000000000000000000 ) ) ;
#1776=EDGE_CURVE ( 'NONE', #5852, #7349, #11238, .T. ) ;
#1778=CARTESIAN_POINT ( 'NONE',  ( 5.284804376168109386, -3.015249596956831368, -4.666192694417973463 ) ) ;
#1787=DIRECTION ( 'NONE',  ( 0.000000000000000000, -8.482162385747133845E-47, 1.000000000000000000 ) ) ;
#1844=EDGE_CURVE ( 'NONE', #6870, #2629, #3742, .T. ) ;
#1848=CARTESIAN_POINT ( 'NONE',  ( -0.1702248550645402425, -5.871782057790573717, -4.589066185948686538 ) ) ;
#1850=ORIENTED_EDGE ( 'NONE', *, *, #9598, .F. ) ;
#1866=CARTESIAN_POINT ( 'NONE',  ( 3.903127820947815962E-15, 5.773502691896270633, -0.5999999999999894307 ) ) ;
#1868=AXIS2_PLACEMENT_3D ( 'NONE', #9436, #2790, #7226 ) ;
#1891=ORIENTED_EDGE ( 'NONE', *, *, #3210, .F. ) ;
#1892=ORIENTED_EDGE ( 'NONE', *, *, #12248, .T. ) ;
#1921=ADVANCED_FACE ( 'NONE', ( #11186 ), #12517, .F. ) ;
#1982=( BOUNDED_SURFACE ( )  B_SPLINE_SURFACE ( 3, 2, ( 
 ( #6467, #10941, #5380 ),
 ( #990, #9849, #14325 ),
 ( #5454, #14395, #11154 ),
 ( #6965, #8884, #5656 ),
 ( #12475, #12534, #4524 ),
 ( #10195, #5718, #8063 ) ),
 .UNSPECIFIED., .F., .F., .T. ) 
 B_SPLINE_SURFACE_WITH_KNOTS ( ( 4, 2, 4 ),
 ( 3, 3 ),
 ( 0.002450104044831662078, 0.005591829551853649133, 0.008733555058875635754 ),
 ( 0.000000000000000000, 1.000000000000000000 ),
 .UNSPECIFIED. ) 
 GEOMETRIC_REPRESENTATION_ITEM ( )  RATIONAL_B_SPLINE_SURFACE ( (
 ( 1.000000000000000000, 0.8047731410850403888, 1.000000000000000000),
 ( 1.000000000000000000, 0.8125552299157110525, 1.000000000000000000),
 ( 1.000000000000000000, 0.8191520442888688969, 1.000000000000000000),
 ( 1.000000000000000000, 0.8191520442891042642, 1.000000000000000000),
 ( 1.000000000000000000, 0.8125552299155337499, 1.000000000000000000),
 ( 1.000000000000000000, 0.8047731410850403888, 1.000000000000000000) ) ) 
 REPRESENTATION_ITEM ( '' )  SURFACE ( )  );
#2014=CARTESIAN_POINT ( 'NONE',  ( 5.253368672218637236, -3.033033817057797510, -4.659491423763650886 ) ) ;
#2023=CARTESIAN_POINT ( 'NONE',  ( -2.500000000000000444, 3.775608651740452848E-15, -0.3501037691048258793 ) ) ;
#2029=ADVANCED_FACE ( 'NONE', ( #13912 ), #9800, .T. ) ;
#2048=CARTESIAN_POINT ( 'NONE',  ( -5.000000000000000000, 2.886751345948124214, -4.284345921091780696 ) ) ;
#2061=DIRECTION ( 'NONE',  ( -1.000000000000000000, 0.000000000000000000, 0.000000000000000000 ) ) ;
#2118=AXIS2_PLACEMENT_3D ( 'NONE', #5069, #7337, #3911 ) ;
#2134=SURFACE_STYLE_FILL_AREA ( #10975 ) ;
#2157=CARTESIAN_POINT ( 'NONE',  ( 5.000000000000001776, 2.886751345948120662, -4.284345921091780696 ) ) ;
#2194=EDGE_CURVE ( 'NONE', #11372, #8941, #9136, .T. ) ;
#2207=DIRECTION ( 'NONE',  ( 1.000000000000000000, 0.000000000000000000, 0.000000000000000000 ) ) ;
#2225=CARTESIAN_POINT ( 'NONE',  ( -2.500000000000000444, 3.775608651740452848E-15, -6.000000000000005329 ) ) ;
#2248=CARTESIAN_POINT ( 'NONE',  ( 3.370256023960729782E-15, 5.773502691896274186, -4.284345921091780696 ) ) ;
#2286=DIRECTION ( 'NONE',  ( 0.000000000000000000, -8.482162385747133845E-47, 1.000000000000000000 ) ) ;
#2301=DIRECTION ( 'NONE',  ( 0.000000000000000000, -8.482162385747133845E-47, 1.000000000000000000 ) ) ;
#2307=LINE ( 'NONE', #10060, #4427 ) ;
#2308=DIRECTION ( 'NONE',  ( -0.000000000000000000, -8.482162385747133845E-47, 1.000000000000000000 ) ) ;
#2320=VERTEX_POINT ( 'NONE', #13178 ) ;
#2323=CARTESIAN_POINT ( 'NONE',  ( 5.000000000000001776, -3.130589478369270928, -4.327780579809764383 ) ) ;
#2328=CARTESIAN_POINT ( 'NONE',  ( 2.500000000000011546, -4.330127018922186544, 0.000000000000000000 ) ) ;
#2337=CARTESIAN_POINT ( 'NONE',  ( 1.738521435313293395, -5.045405839192998343, -4.385926550512764699 ) ) ;
#2358=EDGE_CURVE ( 'NONE', #9831, #10243, #11943, .T. ) ;
#2365=AXIS2_PLACEMENT_3D ( 'NONE', #14253, #2308, #14397 ) ;
#2372=STYLED_ITEM ( 'NONE', ( #7456 ), #11496 ) ;
#2385=AXIS2_PLACEMENT_3D ( 'NONE', #6992, #10437, #8307 ) ;
#2409=EDGE_LOOP ( 'NONE', ( #7696, #2977, #9012, #13717 ) ) ;
#2425=ORIENTED_EDGE ( 'NONE', *, *, #8136, .F. ) ;
#2427=ADVANCED_FACE ( 'NONE', ( #11319 ), #4044, .F. ) ;
#2441=ADVANCED_FACE ( 'NONE', ( #10367 ), #8373, .T. ) ;
#2461=EDGE_LOOP ( 'NONE', ( #5924, #11778, #11236, #6216, #155 ) ) ;
#2466=CARTESIAN_POINT ( 'NONE',  ( 5.000000000000001776, -1.069734140705724146, -4.273127864870867931 ) ) ;
#2482=CARTESIAN_POINT ( 'NONE',  ( -5.000000000000000000, 2.886751345948124214, -0.5999999999999894307 ) ) ;
#2484=PLANE ( 'NONE',  #4019 ) ;
#2487=EDGE_CURVE ( 'NONE', #14260, #13012, #1468, .T. ) ;
#2501=EDGE_CURVE ( 'NONE', #7349, #8967, #4648, .T. ) ;
#2525=ADVANCED_FACE ( 'NONE', ( #13822 ), #9745, .T. ) ;
#2550=CARTESIAN_POINT ( 'NONE',  ( 5.000000000000000000, -2.886751345948152192, -0.5999999999999894307 ) ) ;
#2574=PRODUCT_DEFINITION ( 'UNKNOWN', '', #9674, #3673 ) ;
#2580=AXIS2_PLACEMENT_3D ( 'NONE', #6611, #8745, #11151 ) ;
#2581=ORIENTED_EDGE ( 'NONE', *, *, #6981, .T. ) ;
#2584=FACE_OUTER_BOUND ( 'NONE', #3768, .T. ) ;
#2588=CARTESIAN_POINT ( 'NONE',  ( -5.248988766908546211, 2.532174945215636797, -4.566961984436638922 ) ) ;
#2593=VECTOR ( 'NONE', #5356, 1000.000000000000000 ) ;
#2625=VERTEX_POINT ( 'NONE', #2023 ) ;
#2629=VERTEX_POINT ( 'NONE', #10734 ) ;
#2632=EDGE_CURVE ( 'NONE', #6805, #8967, #3709, .T. ) ;
#2643=PRODUCT ( 'hex flange nut gradea_iso_ISO - 4161 - M6 - N', 'hex flange nut gradea_iso_ISO - 4161 - M6 - N', '', ( #9658 ) ) ;
#2655=ORIENTED_EDGE ( 'NONE', *, *, #2194, .F. ) ;
#2679=DIRECTION ( 'NONE',  ( 0.000000000000000000, 8.482162385747133845E-47, -1.000000000000000000 ) ) ;
#2709=CARTESIAN_POINT ( 'NONE',  ( 0.000000000000000000, 0.000000000000000000, 0.000000000000000000 ) ) ;
#2790=DIRECTION ( 'NONE',  ( 0.5000000000000022204, -0.8660254037844373753, -8.404057939144332757E-32 ) ) ;
#2825=CARTESIAN_POINT ( 'NONE',  ( -5.000000000000001776, -2.886751345948152192, -0.5999999999999894307 ) ) ;
#2848=B_SPLINE_CURVE_WITH_KNOTS ( 'NONE', 3,
 ( #4125, #6142, #10759, #12978, #7385, #9663, #13992, #1608, #3891, #6286 ),
 .UNSPECIFIED., .F., .F.,
 ( 4, 2, 2, 2, 4 ),
 ( 1.451678239244173839E-19, 0.001528561485809837566, 0.003057122971619674699, 0.004585684457429510530, 0.006114245943239346795 ),
 .UNSPECIFIED. ) ;
#2857=ADVANCED_FACE ( 'NONE', ( #4523 ), #1034, .F. ) ;
#2887=CARTESIAN_POINT ( 'NONE',  ( 4.319324222800735136, -3.279739689145003467, -4.138711833384554950 ) ) ;
#2888=CARTESIAN_POINT ( 'NONE',  ( -0.8441225671336188840, -5.568793373799661772, -4.476900509771287062 ) ) ;
#2923=CIRCLE ( 'NONE', #10839, 5.000000000000000888 ) ;
#2953=CARTESIAN_POINT ( 'NONE',  ( 2.999999999999986233, -3.266600723550367725E-47, 5.421010862427522170E-17 ) ) ;
#2957=CARTESIAN_POINT ( 'NONE',  ( 0.6806757771989077055, -5.380514348699644955, -4.138711833382306082 ) ) ;
#2977=ORIENTED_EDGE ( 'NONE', *, *, #3326, .T. ) ;
#2986=VECTOR ( 'NONE', #2286, 1000.000000000000000 ) ;
#3000=CARTESIAN_POINT ( 'NONE',  ( 2.931639317407903178, -4.080919942823946656, -0.01465562841809697585 ) ) ;
#3031=( NAMED_UNIT ( * ) SI_UNIT ( $, .STERADIAN. ) SOLID_ANGLE_UNIT ( ) );
#3033=B_SPLINE_CURVE_WITH_KNOTS ( 'NONE', 3,
 ( #13828, #12497, #4880, #13751, #9341 ),
 .UNSPECIFIED., .F., .F.,
 ( 4, 1, 4 ),
 ( 6.279784878834692592E-20, 0.002886751345948135490, 0.005773502691896270980 ),
 .UNSPECIFIED. ) ;
#3045=CARTESIAN_POINT ( 'NONE',  ( 5.000000000000001776, 2.886751345948120662, -4.284345921091780696 ) ) ;
#3058=ORIENTED_EDGE ( 'NONE', *, *, #8113, .F. ) ;
#3061=VERTEX_POINT ( 'NONE', #7752 ) ;
#3094=CIRCLE ( 'NONE', #3782, 2.500000000000000444 ) ;
#3112=CARTESIAN_POINT ( 'NONE',  ( 5.236872748402768174, 0.5087250997262710017, -4.357689166958468086 ) ) ;
#3148=CARTESIAN_POINT ( 'NONE',  ( 4.597743007729421905, 3.118994528718957771, -0.4198507760575558301 ) ) ;
#3159=ADVANCED_FACE ( 'NONE', ( #11654 ), #14158, .F. ) ;
#3164=B_SPLINE_CURVE_WITH_KNOTS ( 'NONE', 3,
 ( #9605, #4071, #12093, #9685, #821, #4289 ),
 .UNSPECIFIED., .F., .F.,
 ( 4, 2, 4 ),
 ( -3.988673288087340225E-06, 0.0002483701411510689508, 0.0005007289555902253103 ),
 .UNSPECIFIED. ) ;
#3177=CARTESIAN_POINT ( 'NONE',  ( -5.000000000000001776, -2.886751345948141534, -6.000000000000005329 ) ) ;
#3194=ORIENTED_EDGE ( 'NONE', *, *, #2487, .F. ) ;
#3203=CARTESIAN_POINT ( 'NONE',  ( -3.000000000000000888, 3.469446951953614189E-15, -5.974599999999997024 ) ) ;
#3210=EDGE_CURVE ( 'NONE', #7073, #12268, #11811, .T. ) ;
#3223=ORIENTED_EDGE ( 'NONE', *, *, #1236, .T. ) ;
#3229=CIRCLE ( 'NONE', #9295, 3.000000000000000888 ) ;
#3231=CARTESIAN_POINT ( 'NONE',  ( -5.000000000000000000, 1.231908430319618164, -0.1119772403577083270 ) ) ;
#3289=CARTESIAN_POINT ( 'NONE',  ( 5.000000000000000000, -2.886751345948152192, -0.5999999999999894307 ) ) ;
#3294=CIRCLE ( 'NONE', #12398, 5.000000000000000888 ) ;
#3305=PRESENTATION_STYLE_ASSIGNMENT (( #7665 ) ) ;
#3307=CARTESIAN_POINT ( 'NONE',  ( -3.060208875726627031, 4.280211771583977587, -4.357749648769113193 ) ) ;
#3312=DIRECTION ( 'NONE',  ( 0.5000000000000036637, 0.8660254037844365982, -8.404057939144371073E-32 ) ) ;
#3319=COLOUR_RGB ( '', 0.09019608, 0.27058824, 0.51372549) ;
#3326=EDGE_CURVE ( 'NONE', #6044, #2625, #4210, .T. ) ;
#3344=CARTESIAN_POINT ( 'NONE',  ( -2.999999999999986233, 3.673940397442042119E-16, 5.421010862427522170E-17 ) ) ;
#3367=B_SPLINE_CURVE_WITH_KNOTS ( 'NONE', 3,
 ( #4301, #7780, #8805, #10926, #11081 ),
 .UNSPECIFIED., .F., .F.,
 ( 4, 1, 4 ),
 ( 5.651806390950781813E-20, 0.002886751345948135924, 0.005773502691896271848 ),
 .UNSPECIFIED. ) ;
#3368=CARTESIAN_POINT ( 'NONE',  ( -5.000000000000000888, 0.000000000000000000, 0.000000000000000000 ) ) ;
#3371=DIRECTION ( 'NONE',  ( -1.000000000000000000, 0.000000000000000000, 0.000000000000000000 ) ) ;
#3384=CARTESIAN_POINT ( 'NONE',  ( -4.817220356105915258, 3.279784343982800277, -4.566919140436430880 ) ) ;
#3387=CARTESIAN_POINT ( 'NONE',  ( 0.000000000000000000, 0.000000000000000000, -0.3851141460153306717 ) ) ;
#3422=VERTEX_POINT ( 'NONE', #7282 ) ;
#3435=LINE ( 'NONE', #137, #13815 ) ;
#3436=CARTESIAN_POINT ( 'NONE',  ( 6.726859516510133474, 4.293249649474419215E-15, -4.900000000000015454 ) ) ;
#3458=CARTESIAN_POINT ( 'NONE',  ( 3.370256023960729782E-15, 5.773502691896274186, -4.284345921091780696 ) ) ;
#3492=VERTEX_POINT ( 'NONE', #4872 ) ;
#3514=EDGE_LOOP ( 'NONE', ( #4060, #13471, #10647, #12366 ) ) ;
#3534=ORIENTED_EDGE ( 'NONE', *, *, #13005, .T. ) ;
#3574=CARTESIAN_POINT ( 'NONE',  ( 0.000000000000000000, 0.000000000000000000, 0.000000000000000000 ) ) ;
#3575=ORIENTED_EDGE ( 'NONE', *, *, #4447, .T. ) ;
#3587=CYLINDRICAL_SURFACE ( 'NONE', #2385, 2.500000000000000444 ) ;
#3611=EDGE_CURVE ( 'NONE', #8333, #11237, #7170, .T. ) ;
#3647=CARTESIAN_POINT ( 'NONE',  ( 5.000000000000001776, 3.131513003882766988, -4.327950126012554577 ) ) ;
#3652=CARTESIAN_POINT ( 'NONE',  ( 0.8144415599836820618, -5.303284638000498319, -0.2680587191991398166 ) ) ;
#3663=CARTESIAN_POINT ( 'NONE',  ( 5.000000000000003553, 2.886751345948121106, -4.369522543421430427 ) ) ;
#3673=PRODUCT_DEFINITION_CONTEXT ( 'detailed design', #12047, 'design' ) ;
#3676=DIRECTION ( 'NONE',  ( 0.000000000000000000, 8.482162385747133845E-47, -1.000000000000000000 ) ) ;
#3692=CARTESIAN_POINT ( 'NONE',  ( -5.238715782502661789, 1.018209582082211906, -4.386015505371675616 ) ) ;
#3699=CARTESIAN_POINT ( 'NONE',  ( -3.081487911019577365E-30, 3.469446951953614189E-15, -6.000000000000005329 ) ) ;
#3703=CARTESIAN_POINT ( 'NONE',  ( -3.000000000000000888, 3.836840991697820422E-15, -6.000000000000005329 ) ) ;
#3709=CIRCLE ( 'NONE', #4194, 0.5671001622691687061 ) ;
#3742=B_SPLINE_CURVE_WITH_KNOTS ( 'NONE', 3,
 ( #11120, #6367, #6430, #12080, #7822, #10900, #7595, #5551 ),
 .UNSPECIFIED., .F., .F.,
 ( 4, 2, 2, 4 ),
 ( 0.007260997678543217211, 0.007995810154593266036, 0.008730622630643315729, 0.01020024758274341338 ),
 .UNSPECIFIED. ) ;
#3747=CARTESIAN_POINT ( 'NONE',  ( -1.532072935877364915E-15, -6.066067634115591467, -4.659491423763650886 ) ) ;
#3768=EDGE_LOOP ( 'NONE', ( #1891, #10744, #1509, #5493, #8172 ) ) ;
#3782=AXIS2_PLACEMENT_3D ( 'NONE', #7673, #12447, #1102 ) ;
#3784=CARTESIAN_POINT ( 'NONE',  ( -3.081487911019577365E-30, 3.469446951953614189E-15, -4.900000000000015454 ) ) ;
#3794=CARTESIAN_POINT ( 'NONE',  ( 6.532899837730830939, 3.469446951953614189E-15, -6.000000000000005329 ) ) ;
#3813=DIRECTION ( 'NONE',  ( -1.000000000000000000, 0.000000000000000000, 0.000000000000000000 ) ) ;
#3838=CARTESIAN_POINT ( 'NONE',  ( -5.211749180171794116, -2.764497899775275602, -4.327903350935043747 ) ) ;
#3869=DIRECTION ( 'NONE',  ( 0.000000000000000000, 8.482162385747133845E-47, -1.000000000000000000 ) ) ;
#3873=CARTESIAN_POINT ( 'NONE',  ( -0.4012132626380665590, -5.541862106709760205, -0.4203182062997351531 ) ) ;
#3875=ORIENTED_EDGE ( 'NONE', *, *, #6043, .T. ) ;
#3888=LINE ( 'NONE', #8403, #8466 ) ;
#3890=EDGE_CURVE ( 'NONE', #1128, #11372, #12840, .T. ) ;
#3891=CARTESIAN_POINT ( 'NONE',  ( 4.817183509279845843, 3.279805190042297536, -4.566911319714219708 ) ) ;
#3902=CARTESIAN_POINT ( 'NONE',  ( -1.721886139900566270, -5.052888355618796901, -4.357689166958457427 ) ) ;
#3905=CARTESIAN_POINT ( 'NONE',  ( -5.029394918168160089, -2.903722509865338530, -4.451004066889660216 ) ) ;
#3910=ORIENTED_EDGE ( 'NONE', *, *, #8113, .T. ) ;
#3911=DIRECTION ( 'NONE',  ( -1.000000000000000000, 0.000000000000000000, 0.000000000000000000 ) ) ;
#3921=CARTESIAN_POINT ( 'NONE',  ( -6.726859516510170778, 4.293249649474423948E-15, -4.900000000000015454 ) ) ;
#3958=AXIS2_PLACEMENT_3D ( 'NONE', #7060, #13745, #10512 ) ;
#3997=CARTESIAN_POINT ( 'NONE',  ( 2.285412292771018983, 4.454019289455643182, -8.322945739720751976E-15 ) ) ;
#4019=AXIS2_PLACEMENT_3D ( 'NONE', #13769, #8321, #4759 ) ;
#4044=( BOUNDED_SURFACE ( )  B_SPLINE_SURFACE ( 3, 2, ( 
 ( #2323, #9185, #1289 ),
 ( #4668, #7944, #9108 ),
 ( #13682, #2466, #11246 ),
 ( #10075, #4603, #13606 ),
 ( #9037, #6915, #11382 ),
 ( #3647, #13528, #274 ) ),
 .UNSPECIFIED., .F., .F., .F. ) 
 B_SPLINE_SURFACE_WITH_KNOTS ( ( 4, 2, 4 ),
 ( 3, 3 ),
 ( 0.02462021979145854675, 0.02768763742058376331, 0.03075505504970898335 ),
 ( 0.000000000000000000, 1.000000000000000000 ),
 .UNSPECIFIED. ) 
 GEOMETRIC_REPRESENTATION_ITEM ( )  RATIONAL_B_SPLINE_SURFACE ( (
 ( 1.000000000000000000, 0.8047781263388831263, 1.000000000000000000),
 ( 1.000000000000000000, 0.8123781044083938641, 1.000000000000000000),
 ( 1.000000000000000000, 0.8190664127994971011, 1.000000000000000000),
 ( 1.000000000000000000, 0.8192359367744610488, 1.000000000000000000),
 ( 1.000000000000000000, 0.8126133147547173197, 1.000000000000000000),
 ( 1.000000000000000000, 0.8047712418670134316, 1.000000000000000000) ) ) 
 REPRESENTATION_ITEM ( '' )  SURFACE ( )  );
#4045=AXIS2_PLACEMENT_3D ( 'NONE', #14105, #5077, #11749 ) ;
#4058=SHAPE_REPRESENTATION_RELATIONSHIP ( 'NONE' , 'NONE' ,  #4961, #11496 ) ;
#4060=ORIENTED_EDGE ( 'NONE', *, *, #11713, .T. ) ;
#4067=CIRCLE ( 'NONE', #540, 3.000000000000000888 ) ;
#4071=CARTESIAN_POINT ( 'NONE',  ( -5.184911785341500767, 2.993510214989689722, -4.630720594357042863 ) ) ;
#4086=AXIS2_PLACEMENT_3D ( 'NONE', #5968, #7071, #7140 ) ;
#4101=DIRECTION ( 'NONE',  ( 0.000000000000000000, 0.000000000000000000, -1.000000000000000000 ) ) ;
#4113=ORIENTED_EDGE ( 'NONE', *, *, #8262, .F. ) ;
#4125=CARTESIAN_POINT ( 'NONE',  ( 3.667453972563985829E-15, 6.066067634115573703, -4.659491423763650886 ) ) ;
#4130=DIRECTION ( 'NONE',  ( 1.224646799147353207E-16, 1.000000000000000000, 8.482162385747133845E-47 ) ) ;
#4131=FILL_AREA_STYLE_COLOUR ( '', #3319 ) ;
#4132=EDGE_LOOP ( 'NONE', ( #1146, #9603, #5796, #462 ) ) ;
#4135=CARTESIAN_POINT ( 'NONE',  ( -4.319324222800883462, -3.279739689144915538, -4.138711833383139194 ) ) ;
#4154=DIRECTION ( 'NONE',  ( 1.000000000000000000, 0.000000000000000000, 0.000000000000000000 ) ) ;
#4194=AXIS2_PLACEMENT_3D ( 'NONE', #13226, #12189, #4101 ) ;
#4200=EDGE_CURVE ( 'NONE', #13012, #8333, #12318, .T. ) ;
#4201=( NAMED_UNIT ( * ) PLANE_ANGLE_UNIT ( ) SI_UNIT ( $, .RADIAN. ) );
#4202=( GEOMETRIC_REPRESENTATION_CONTEXT ( 3 ) GLOBAL_UNCERTAINTY_ASSIGNED_CONTEXT ( ( #1331 ) ) GLOBAL_UNIT_ASSIGNED_CONTEXT ( ( #10231, #1025, #6793 ) ) REPRESENTATION_CONTEXT ( 'NONE', 'WORKASPACE' ) );
#4205=CARTESIAN_POINT ( 'NONE',  ( -2.241758896820161572E-14, 5.987020429981935621, -4.630720594357044639 ) ) ;
#4210=LINE ( 'NONE', #2225, #2986 ) ;
#4234=FACE_OUTER_BOUND ( 'NONE', #3514, .T. ) ;
#4248=AXIS2_PLACEMENT_3D ( 'NONE', #3784, #12545, #10358 ) ;
#4254=CARTESIAN_POINT ( 'NONE',  ( 5.248988766908546211, -2.532174945215656336, -4.566961984436638033 ) ) ;
#4259=CIRCLE ( 'NONE', #12892, 3.000000000000000888 ) ;
#4273=CARTESIAN_POINT ( 'NONE',  ( 3.667453972563985829E-15, 6.066067634115573703, -4.659491423763650886 ) ) ;
#4289=CARTESIAN_POINT ( 'NONE',  ( -5.000000000000000000, 2.886751345948124214, -4.284345921091780696 ) ) ;
#4301=CARTESIAN_POINT ( 'NONE',  ( 3.370256023960729782E-15, 5.773502691896274186, -4.284345921091780696 ) ) ;
#4303=CARTESIAN_POINT ( 'NONE',  ( 5.122341571230614399, -2.957385285031222111, -4.581776566113600957 ) ) ;
#4342=CARTESIAN_POINT ( 'NONE',  ( -3.499999647538288627, 4.028415724610453275, -4.385927688751848130 ) ) ;
#4384=DIRECTION ( 'NONE',  ( 0.8191520442889913545, -4.865168473767734750E-47, 0.5735764363510468256 ) ) ;
#4388=APPLICATION_CONTEXT ( 'automotive_design' ) ;
#4397=CARTESIAN_POINT ( 'NONE',  ( 6.726859516510170778, 3.469446951953614189E-15, -4.900000000000015454 ) ) ;
#4412=CARTESIAN_POINT ( 'NONE',  ( 3.499999647538293956, -4.028415724610476367, -4.385927688751854348 ) ) ;
#4427=VECTOR ( 'NONE', #10265, 1000.000000000000000 ) ;
#4447=EDGE_CURVE ( 'NONE', #10332, #6697, #232, .T. ) ;
#4457=AXIS2_PLACEMENT_3D ( 'NONE', #9749, #14301, #14375 ) ;
#4465=DIRECTION ( 'NONE',  ( 1.000000000000000000, 0.000000000000000000, 0.000000000000000000 ) ) ;
#4477=ORIENTED_EDGE ( 'NONE', *, *, #11688, .T. ) ;
#4484=CARTESIAN_POINT ( 'NONE',  ( -5.000000000000001776, 1.953108124182664440, -0.2699991669428312147 ) ) ;
#4498=CARTESIAN_POINT ( 'NONE',  ( -3.081487911019577365E-30, 3.469446951953614189E-15, -6.000000000000005329 ) ) ;
#4501=EDGE_CURVE ( 'NONE', #5852, #6805, #11041, .T. ) ;
#4516=EDGE_CURVE ( 'NONE', #10243, #10813, #13703, .T. ) ;
#4523=FACE_OUTER_BOUND ( 'NONE', #10701, .T. ) ;
#4524=CARTESIAN_POINT ( 'NONE',  ( -0.6806757772000455731, 5.380514348698967275, -4.138711833383633909 ) ) ;
#4541=CARTESIAN_POINT ( 'NONE',  ( -5.000000000000000000, -0.9835753746177068324, -0.05800540215398777844 ) ) ;
#4544=DIRECTION ( 'NONE',  ( 0.000000000000000000, -8.482162385747133845E-47, 1.000000000000000000 ) ) ;
#4567=ORIENTED_EDGE ( 'NONE', *, *, #6072, .T. ) ;
#4603=CARTESIAN_POINT ( 'NONE',  ( 5.000000000000001776, 1.026510551521092385, -4.269855120319423492 ) ) ;
#4615=CARTESIAN_POINT ( 'NONE',  ( 0.4318028594007592424, -5.811705888749004956, -4.566911319714220596 ) ) ;
#4617=CARTESIAN_POINT ( 'NONE',  ( -5.236775389869354314, -1.020994252193095253, -4.356146547543389147 ) ) ;
#4619=AXIS2_PLACEMENT_3D ( 'NONE', #8664, #13007, #4154 ) ;
#4631=EDGE_CURVE ( 'NONE', #3492, #1128, #13010, .T. ) ;
#4632=CARTESIAN_POINT ( 'NONE',  ( -1.752700365193367750E-15, -5.773502691896304384, -4.284345921091780696 ) ) ;
#4646=DIRECTION ( 'NONE',  ( -1.000000000000000000, 0.000000000000000000, 0.000000000000000000 ) ) ;
#4648=CIRCLE ( 'NONE', #3958, 6.726859516510133474 ) ;
#4654=CARTESIAN_POINT ( 'NONE',  ( 0.000000000000000000, 0.000000000000000000, -0.3851141460153306717 ) ) ;
#4662=ORIENTED_EDGE ( 'NONE', *, *, #11245, .T. ) ;
#4666=CARTESIAN_POINT ( 'NONE',  ( -3.081487911019577365E-30, 3.469446951953614189E-15, -5.432899837730820636 ) ) ;
#4668=CARTESIAN_POINT ( 'NONE',  ( 5.000000000000001776, -2.119125225736587570, -4.142110484952109317 ) ) ;
#4673=DIRECTION ( 'NONE',  ( -1.000000000000000000, 0.000000000000000000, 0.000000000000000000 ) ) ;
#4675=FACE_OUTER_BOUND ( 'NONE', #5880, .T. ) ;
#4683=ORIENTED_EDGE ( 'NONE', *, *, #12732, .T. ) ;
#4687=CARTESIAN_POINT ( 'NONE',  ( -5.000000000000000000, -1.044998857007659154, -4.017857204714943897 ) ) ;
#4710=CARTESIAN_POINT ( 'NONE',  ( -5.000000000000001776, -2.886751345948152192, -4.284345921091780696 ) ) ;
#4728=AXIS2_PLACEMENT_3D ( 'NONE', #14203, #1604, #8486 ) ;
#4735=DIRECTION ( 'NONE',  ( 0.000000000000000000, 8.482162385747133845E-47, -1.000000000000000000 ) ) ;
#4748=CARTESIAN_POINT ( 'NONE',  ( 5.000000000000001776, -0.4954705650270038175, -7.013432803265606807E-16 ) ) ;
#4759=DIRECTION ( 'NONE',  ( -1.000000000000000000, 0.000000000000000000, 0.000000000000000000 ) ) ;
#4786=CARTESIAN_POINT ( 'NONE',  ( -4.597743007729438780, -3.118994528718963988, -0.4198507760575687642 ) ) ;
#4789=CARTESIAN_POINT ( 'NONE',  ( -0.1702248550645321934, 5.871782057790553289, -4.589066185948677656 ) ) ;
#4827=ORIENTED_EDGE ( 'NONE', *, *, #1236, .F. ) ;
#4829=ORIENTED_EDGE ( 'NONE', *, *, #11688, .F. ) ;
#4855=CARTESIAN_POINT ( 'NONE',  ( 1.721886139900248969, 5.052888355619074900, -4.357689166958493843 ) ) ;
#4872=CARTESIAN_POINT ( 'NONE',  ( 5.000000000000001776, 2.886751345948120662, -4.284345921091780696 ) ) ;
#4874=ADVANCED_FACE ( 'NONE', ( #4234 ), #14221, .F. ) ;
#4880=CARTESIAN_POINT ( 'NONE',  ( 2.499999999999997780, -4.330127018922222959, -3.920524600599856413 ) ) ;
#4921=B_SPLINE_CURVE_WITH_KNOTS ( 'NONE', 3,
 ( #14223, #4205, #12026, #8643, #13133, #3458 ),
 .UNSPECIFIED., .F., .F.,
 ( 4, 2, 4 ),
 ( -3.988673288090718192E-06, 0.0002483701411510679750, 0.0005007289555902266114 ),
 .UNSPECIFIED. ) ;
#4926=CARTESIAN_POINT ( 'NONE',  ( -5.236872748402763733, 0.5081686017868803917, -4.357689166958460980 ) ) ;
#4940=AXIS2_PLACEMENT_3D ( 'NONE', #10891, #1760, #10753 ) ;
#4956=FACE_OUTER_BOUND ( 'NONE', #13251, .T. ) ;
#4958=DIRECTION ( 'NONE',  ( 0.000000000000000000, -8.482162385747133845E-47, 1.000000000000000000 ) ) ;
#4961=SHAPE_REPRESENTATION ( 'hex flange nut gradea_iso_ISO - 4161 - M6 - N', ( #11025 ), #5842 ) ;
#4962=AXIS2_PLACEMENT_3D ( 'NONE', #5912, #10394, #372 ) ;
#4970=FACE_OUTER_BOUND ( 'NONE', #384, .T. ) ;
#4994=VERTEX_POINT ( 'NONE', #13445 ) ;
#5015=CARTESIAN_POINT ( 'NONE',  ( 1.642566673137918487, 4.825166380998191507, -0.07080520455422339987 ) ) ;
#5059=DIRECTION ( 'NONE',  ( -1.000000000000000000, 0.000000000000000000, 0.000000000000000000 ) ) ;
#5065=DIRECTION ( 'NONE',  ( -0.5000000000000024425, 0.8660254037844373753, 8.404057939144334946E-32 ) ) ;
#5069=CARTESIAN_POINT ( 'NONE',  ( -3.081487911019577365E-30, 3.469446951953614189E-15, -5.974599999999997024 ) ) ;
#5072=CARTESIAN_POINT ( 'NONE',  ( 1.598077599629971202, 4.850852159564532862, -4.271474537231044089 ) ) ;
#5073=DIRECTION ( 'NONE',  ( -0.9396926207859143121, 2.901070394884691809E-47, -0.3420201433256522816 ) ) ;
#5077=DIRECTION ( 'NONE',  ( 0.000000000000000000, -8.482162385747133845E-47, 1.000000000000000000 ) ) ;
#5099=CARTESIAN_POINT ( 'NONE',  ( 3.567687560464438246, -3.713697318477663600, -0.1121614189353530300 ) ) ;
#5146=CARTESIAN_POINT ( 'NONE',  ( 4.166666666666669627, 3.367876570272813730, -4.118275046351175916 ) ) ;
#5164=AXIS2_PLACEMENT_3D ( 'NONE', #4654, #12604, #7929 ) ;
#5209=CARTESIAN_POINT ( 'NONE',  ( 1.598077599630167711, -4.850852159564259303, -4.271474537231044089 ) ) ;
#5225=ORIENTED_EDGE ( 'NONE', *, *, #7390, .F. ) ;
#5238=ORIENTED_EDGE ( 'NONE', *, *, #1844, .T. ) ;
#5247=FACE_OUTER_BOUND ( 'NONE', #12911, .T. ) ;
#5296=FACE_OUTER_BOUND ( 'NONE', #2409, .T. ) ;
#5321=CARTESIAN_POINT ( 'NONE',  ( 2.930059260563453005, 4.081832189068404837, -8.080694316806025235E-15 ) ) ;
#5330=SHAPE_DEFINITION_REPRESENTATION ( #5759, #4961 ) ;
#5349=EDGE_LOOP ( 'NONE', ( #11109, #9631, #13994, #3194 ) ) ;
#5356=DIRECTION ( 'NONE',  ( 0.000000000000000000, -8.482162385747133845E-47, 1.000000000000000000 ) ) ;
#5380=CARTESIAN_POINT ( 'NONE',  ( -5.211749180171795892, 2.764497899775258283, -4.327903350935040194 ) ) ;
#5400=CIRCLE ( 'NONE', #4940, 6.726859516510133474 ) ;
#5419=EDGE_LOOP ( 'NONE', ( #12431, #2655, #7706, #10350, #6054 ) ) ;
#5441=DIRECTION ( 'NONE',  ( 1.000000000000000000, 0.000000000000000000, 0.000000000000000000 ) ) ;
#5454=CARTESIAN_POINT ( 'NONE',  ( -3.514986608503188670, 4.017641317387355748, -4.357689166958564009 ) ) ;
#5458=CARTESIAN_POINT ( 'NONE',  ( -3.567687560464433361, 3.713697318477639620, -0.1121614189353362934 ) ) ;
#5471=CARTESIAN_POINT ( 'NONE',  ( 3.667453972563985829E-15, 6.066067634115573703, -4.659491423763650886 ) ) ;
#5472=FACE_OUTER_BOUND ( 'NONE', #1335, .T. ) ;
#5473=CARTESIAN_POINT ( 'NONE',  ( 5.236872748402767286, 8.765285303662936917E-14, -4.357689166958464533 ) ) ;
#5493=ORIENTED_EDGE ( 'NONE', *, *, #7052, .T. ) ;
#5536=DIRECTION ( 'NONE',  ( 0.000000000000000000, 8.482162385747133845E-47, -1.000000000000000000 ) ) ;
#5551=CARTESIAN_POINT ( 'NONE',  ( 5.000000000000001776, 2.886751345948152192, -0.5999999999999894307 ) ) ;
#5581=CARTESIAN_POINT ( 'NONE',  ( -0.8144415599836899444, 5.303284638000468121, -0.2680587191991168350 ) ) ;
#5601=ORIENTED_EDGE ( 'NONE', *, *, #10428, .T. ) ;
#5604=CARTESIAN_POINT ( 'NONE',  ( -5.000000000000000888, -1.947799557644009694, -0.2684016432552358000 ) ) ;
#5617=VECTOR ( 'NONE', #1230, 1000.000000000000227 ) ;
#5656=CARTESIAN_POINT ( 'NONE',  ( -1.582370436562975380, 4.859920694388930151, -4.019399823475544586 ) ) ;
#5664=EDGE_CURVE ( 'NONE', #641, #2625, #14044, .T. ) ;
#5688=CARTESIAN_POINT ( 'NONE',  ( 3.060208875726633249, -4.280211771583999791, -4.357749648769123851 ) ) ;
#5690=CARTESIAN_POINT ( 'NONE',  ( -5.000000000000000000, -2.094342041905651541, -4.137519424005751567 ) ) ;
#5697=EDGE_LOOP ( 'NONE', ( #4829, #6409 ) ) ;
#5699=ORIENTED_EDGE ( 'NONE', *, *, #4516, .T. ) ;
#5702=FACE_OUTER_BOUND ( 'NONE', #11575, .T. ) ;
#5714=CARTESIAN_POINT ( 'NONE',  ( -4.185558440016327708, -3.356969399843937385, -0.2680587191991219975 ) ) ;
#5718=CARTESIAN_POINT ( 'NONE',  ( 0.1702248550645398539, 5.871782057790552400, -4.589066185948675880 ) ) ;
#5745=EDGE_LOOP ( 'NONE', ( #7096, #7157, #8311, #4477 ) ) ;
#5751=ADVANCED_FACE ( 'NONE', ( #1288 ), #12162, .T. ) ;
#5756=AXIS2_PLACEMENT_3D ( 'NONE', #6192, #13895, #9415 ) ;
#5759=PRODUCT_DEFINITION_SHAPE ( 'NONE', 'NONE',  #2574 ) ;
#5772=AXIS2_PLACEMENT_3D ( 'NONE', #8674, #6463, #12333 ) ;
#5781=CARTESIAN_POINT ( 'NONE',  ( -0.4022569922705768186, 5.541259509125445071, -0.4198507760575658776 ) ) ;
#5796=ORIENTED_EDGE ( 'NONE', *, *, #13715, .F. ) ;
#5799=DIRECTION ( 'NONE',  ( -1.000000000000000000, 0.000000000000000000, 0.000000000000000000 ) ) ;
#5819=EDGE_CURVE ( 'NONE', #3492, #2629, #573, .T. ) ;
#5827=DIRECTION ( 'NONE',  ( -0.8191520442889909104, 4.865168473767738639E-47, -0.5735764363510472696 ) ) ;
#5831=CIRCLE ( 'NONE', #12168, 2.500000000000000444 ) ;
#5837=CARTESIAN_POINT ( 'NONE',  ( -1.533718260776178309E-15, -5.773502691896303496, -4.369522543421428651 ) ) ;
#5842=( GEOMETRIC_REPRESENTATION_CONTEXT ( 3 ) GLOBAL_UNCERTAINTY_ASSIGNED_CONTEXT ( ( #11880 ) ) GLOBAL_UNIT_ASSIGNED_CONTEXT ( ( #814, #10768, #3031 ) ) REPRESENTATION_CONTEXT ( 'NONE', 'WORKASPACE' ) );
#5852=VERTEX_POINT ( 'NONE', #11980 ) ;
#5862=FACE_OUTER_BOUND ( 'NONE', #8800, .T. ) ;
#5880=EDGE_LOOP ( 'NONE', ( #1321, #11724, #920, #11834 ) ) ;
#5902=CARTESIAN_POINT ( 'NONE',  ( -5.244721914230359161, -2.047008728252464937, -4.475704751401925030 ) ) ;
#5905=ORIENTED_EDGE ( 'NONE', *, *, #13529, .F. ) ;
#5912=CARTESIAN_POINT ( 'NONE',  ( 0.000000000000000000, 0.000000000000000000, 0.000000000000000000 ) ) ;
#5913=EDGE_CURVE ( 'NONE', #2320, #10194, #7238, .T. ) ;
#5924=ORIENTED_EDGE ( 'NONE', *, *, #13950, .T. ) ;
#5947=ORIENTED_EDGE ( 'NONE', *, *, #499, .F. ) ;
#5968=CARTESIAN_POINT ( 'NONE',  ( -3.081487911019577365E-30, 3.469446951953614189E-15, -6.000000000000005329 ) ) ;
#5977=FACE_OUTER_BOUND ( 'NONE', #11655, .T. ) ;
#5980=CARTESIAN_POINT ( 'NONE',  ( -3.000000000000000888, 3.836840991697820422E-15, -25.03750572909319061 ) ) ;
#6006=CARTESIAN_POINT ( 'NONE',  ( -5.236872748402765509, -8.016972670139777574E-14, -4.357689166958463645 ) ) ;
#6039=CARTESIAN_POINT ( 'NONE',  ( 5.000000000000002665, -1.947799557644007695, -0.2684016432552362441 ) ) ;
#6043=EDGE_CURVE ( 'NONE', #4994, #9831, #6980, .T. ) ;
#6044=VERTEX_POINT ( 'NONE', #12397 ) ;
#6054=ORIENTED_EDGE ( 'NONE', *, *, #7451, .F. ) ;
#6057=CARTESIAN_POINT ( 'NONE',  ( -3.000000000000000888, 3.469446951953614189E-15, -5.974599999999997024 ) ) ;
#6067=CARTESIAN_POINT ( 'NONE',  ( 5.211749180171794116, -2.764497899775278711, -4.327903350935043747 ) ) ;
#6072=EDGE_CURVE ( 'NONE', #13192, #10332, #10494, .T. ) ;
#6084=CARTESIAN_POINT ( 'NONE',  ( 1.582370436563670602, 4.859920694388523366, -4.019399823475544586 ) ) ;
#6090=CARTESIAN_POINT ( 'NONE',  ( 0.8082922630888345061, 5.306834936218050025, -0.2701150775514040703 ) ) ;
#6110=AXIS2_PLACEMENT_3D ( 'NONE', #13336, #3312, #6655 ) ;
#6112=DIRECTION ( 'NONE',  ( 0.000000000000000000, 8.482162385747133845E-47, -1.000000000000000000 ) ) ;
#6130=DIRECTION ( 'NONE',  ( 0.000000000000000000, 8.482162385747133845E-47, -1.000000000000000000 ) ) ;
#6137=EDGE_CURVE ( 'NONE', #11237, #13192, #7685, .T. ) ;
#6142=CARTESIAN_POINT ( 'NONE',  ( 0.4317663827706312851, 5.811727376006665224, -4.566919140436428215 ) ) ;
#6152=VERTEX_POINT ( 'NONE', #9542 ) ;
#6159=ADVANCED_FACE ( 'NONE', ( #11958 ), #10522, .F. ) ;
#6160=AXIS2_PLACEMENT_3D ( 'NONE', #13457, #270, #4465 ) ;
#6167=CARTESIAN_POINT ( 'NONE',  ( -5.236872748402764621, -0.5087250997262708907, -4.357689166958468974 ) ) ;
#6169=ORIENTED_EDGE ( 'NONE', *, *, #13019, .T. ) ;
#6182=EDGE_CURVE ( 'NONE', #3492, #7073, #1418, .T. ) ;
#6192=CARTESIAN_POINT ( 'NONE',  ( 0.000000000000000000, 0.000000000000000000, 0.000000000000000000 ) ) ;
#6193=CARTESIAN_POINT ( 'NONE',  ( 5.000000000000000888, 0.000000000000000000, 0.000000000000000000 ) ) ;
#6216=ORIENTED_EDGE ( 'NONE', *, *, #6072, .F. ) ;
#6225=CARTESIAN_POINT ( 'NONE',  ( 1.721886139900713042, -5.052888355618668115, -4.357689166958440552 ) ) ;
#6237=CARTESIAN_POINT ( 'NONE',  ( 3.370256023960729782E-15, 5.773502691896274186, -4.284345921091780696 ) ) ;
#6254=CYLINDRICAL_SURFACE ( 'NONE', #331, 3.000000000000000888 ) ;
#6255=CARTESIAN_POINT ( 'NONE',  ( -2.176667689905601222, -4.790324513057892197, -4.357749648769125628 ) ) ;
#6286=CARTESIAN_POINT ( 'NONE',  ( 5.253368672218638125, 3.033033817057769532, -4.659491423763650886 ) ) ;
#6315=CONICAL_SURFACE ( 'NONE', #14, 5.000000000000000888, 0.9110539511682884672 ) ;
#6318=EDGE_LOOP ( 'NONE', ( #4827, #10368, #7775, #13080, #3875 ) ) ;
#6357=ADVANCED_FACE ( 'NONE', ( #8938 ), #13434, .T. ) ;
#6367=CARTESIAN_POINT ( 'NONE',  ( 5.000000000000000888, 0.2466074518009269412, -6.594151494374726167E-16 ) ) ;
#6376=CARTESIAN_POINT ( 'NONE',  ( -4.400655246570308599, -3.515428273945673698, -4.476900509771408743 ) ) ;
#6389=ORIENTED_EDGE ( 'NONE', *, *, #12539, .F. ) ;
#6396=CARTESIAN_POINT ( 'NONE',  ( 5.185163620695915299, -2.993655612202863470, -4.630826434870603414 ) ) ;
#6407=ORIENTED_EDGE ( 'NONE', *, *, #12964, .T. ) ;
#6409=ORIENTED_EDGE ( 'NONE', *, *, #8756, .F. ) ;
#6430=CARTESIAN_POINT ( 'NONE',  ( 5.000000000000002665, 0.4965892259340556336, -0.01450341304856543785 ) ) ;
#6440=LINE ( 'NONE', #3177, #2593 ) ;
#6458=FACE_OUTER_BOUND ( 'NONE', #1022, .T. ) ;
#6463=DIRECTION ( 'NONE',  ( 0.000000000000000000, 8.482162385747133845E-47, -1.000000000000000000 ) ) ;
#6467=CARTESIAN_POINT ( 'NONE',  ( -5.284804376168110274, 3.015249596956810940, -4.666192694417969022 ) ) ;
#6480=CARTESIAN_POINT ( 'NONE',  ( 5.244818697407748864, -2.029379090245567063, -4.490884354499014464 ) ) ;
#6488=CARTESIAN_POINT ( 'NONE',  ( -5.000000000000000888, 0.000000000000000000, 0.000000000000000000 ) ) ;
#6524=DIRECTION ( 'NONE',  ( 0.000000000000000000, 0.000000000000000000, 1.000000000000000000 ) ) ;
#6539=ADVANCED_FACE ( 'NONE', ( #4970 ), #10530, .T. ) ;
#6543=CARTESIAN_POINT ( 'NONE',  ( -2.714587707229014324, 4.206234748388740563, -3.210254870093797102E-15 ) ) ;
#6550=AXIS2_PLACEMENT_3D ( 'NONE', #9311, #5065, #14015 ) ;
#6554=DIRECTION ( 'NONE',  ( 1.000000000000000000, 0.000000000000000000, 0.000000000000000000 ) ) ;
#6559=DIRECTION ( 'NONE',  ( 0.000000000000000000, 8.482162385747133845E-47, -1.000000000000000000 ) ) ;
#6567=CARTESIAN_POINT ( 'NONE',  ( -3.081487911019577365E-30, 3.469446951953614189E-15, -5.974599999999997024 ) ) ;
#6601=ORIENTED_EDGE ( 'NONE', *, *, #5913, .F. ) ;
#6611=CARTESIAN_POINT ( 'NONE',  ( 0.000000000000000000, 0.000000000000000000, 0.000000000000000000 ) ) ;
#6648=EDGE_LOOP ( 'NONE', ( #11525, #9649, #3223, #1299, #5699 ) ) ;
#6655=DIRECTION ( 'NONE',  ( -0.8660254037844365982, 0.5000000000000036637, 9.625874682719161934E-32 ) ) ;
#6677=EDGE_LOOP ( 'NONE', ( #10115, #11411, #4113 ) ) ;
#6692=CARTESIAN_POINT ( 'NONE',  ( -4.598786737361986177, 3.118391931134631978, -0.4203182062997263824 ) ) ;
#6697=VERTEX_POINT ( 'NONE', #5471 ) ;
#6701=DIRECTION ( 'NONE',  ( -1.000000000000000000, 0.000000000000000000, 0.000000000000000000 ) ) ;
#6718=VECTOR ( 'NONE', #803, 1000.000000000000000 ) ;
#6720=CARTESIAN_POINT ( 'NONE',  ( -2.179555516819069894, 4.788648424347440979, -4.357628883416061250 ) ) ;
#6721=CARTESIAN_POINT ( 'NONE',  ( -5.000000000000000000, 3.130593237335734802, -4.327781269827185362 ) ) ;
#6757=CARTESIAN_POINT ( 'NONE',  ( 3.000000000000000888, 3.836840991697820422E-15, -5.974599999999997024 ) ) ;
#6758=ORIENTED_EDGE ( 'NONE', *, *, #4501, .T. ) ;
#6773=DIRECTION ( 'NONE',  ( -0.000000000000000000, 8.482162385747133845E-47, -1.000000000000000000 ) ) ;
#6792=ORIENTED_EDGE ( 'NONE', *, *, #8769, .T. ) ;
#6793=( NAMED_UNIT ( * ) SI_UNIT ( $, .STERADIAN. ) SOLID_ANGLE_UNIT ( ) );
#6805=VERTEX_POINT ( 'NONE', #3794 ) ;
#6809=VECTOR ( 'NONE', #13920, 1000.000000000000000 ) ;
#6844=CARTESIAN_POINT ( 'NONE',  ( -5.000000000000001776, -2.886751345948152192, -4.284345921091780696 ) ) ;
#6850=CARTESIAN_POINT ( 'NONE',  ( 2.500000000000000444, 0.000000000000000000, -0.3501037691048258793 ) ) ;
#6870=VERTEX_POINT ( 'NONE', #6193 ) ;
#6904=DIRECTION ( 'NONE',  ( 0.000000000000000000, -8.482162385747133845E-47, 1.000000000000000000 ) ) ;
#6910=MANIFOLD_SOLID_BREP ( 'EndChamfer', #12729 ) ;
#6913=EDGE_LOOP ( 'NONE', ( #7247, #13358, #9406 ) ) ;
#6915=CARTESIAN_POINT ( 'NONE',  ( 5.000000000000001776, 2.068872943223520444, -4.395519625925073726 ) ) ;
#6933=CARTESIAN_POINT ( 'NONE',  ( -5.253679192976075107, 3.068494879228052419, -4.666070613310114190 ) ) ;
#6944=CARTESIAN_POINT ( 'NONE',  ( -5.236872748402765509, -8.016972670139777574E-14, -4.357689166958463645 ) ) ;
#6950=CARTESIAN_POINT ( 'NONE',  ( -4.177163563997814114E-15, -5.807447148981907503, -4.451008977024222268 ) ) ;
#6964=CARTESIAN_POINT ( 'NONE',  ( -0.03111943836865819005, 6.084399642271183239, -4.666192694417976128 ) ) ;
#6965=CARTESIAN_POINT ( 'NONE',  ( -1.721886139899573953, 5.052888355619120198, -4.357689166958383709 ) ) ;
#6974=ORIENTED_EDGE ( 'NONE', *, *, #12964, .F. ) ;
#6980=B_SPLINE_CURVE_WITH_KNOTS ( 'NONE', 3,
 ( #12598, #13661, #7924, #5714, #4786, #11509 ),
 .UNSPECIFIED., .F., .F.,
 ( 4, 2, 4 ),
 ( 0.002950759650825690496, 0.004429055062152287107, 0.005907350473478885020 ),
 .UNSPECIFIED. ) ;
#6981=EDGE_CURVE ( 'NONE', #8941, #8333, #10134, .T. ) ;
#6992=CARTESIAN_POINT ( 'NONE',  ( -3.081487911019577365E-30, 3.469446951953614189E-15, -6.000000000000005329 ) ) ;
#7000=EDGE_CURVE ( 'NONE', #641, #1738, #8963, .T. ) ;
#7006=VECTOR ( 'NONE', #9708, 1000.000000000000000 ) ;
#7035=CARTESIAN_POINT ( 'NONE',  ( -5.253368672218636348, 3.033033817057773085, -4.659491423763650886 ) ) ;
#7037=CARTESIAN_POINT ( 'NONE',  ( 0.6806757771994083051, 5.380514348699340310, -4.138711833382858529 ) ) ;
#7043=CARTESIAN_POINT ( 'NONE',  ( -4.999999999999998224, -1.366094737331735587E-14, -3.920524600599843978 ) ) ;
#7052=EDGE_CURVE ( 'NONE', #10813, #2320, #12058, .T. ) ;
#7060=CARTESIAN_POINT ( 'NONE',  ( -3.081487911019577365E-30, 3.469446951953614189E-15, -4.900000000000015454 ) ) ;
#7071=DIRECTION ( 'NONE',  ( -0.000000000000000000, -8.482162385747133845E-47, 1.000000000000000000 ) ) ;
#7073=VERTEX_POINT ( 'NONE', #2248 ) ;
#7087=ORIENTED_EDGE ( 'NONE', *, *, #2501, .T. ) ;
#7096=ORIENTED_EDGE ( 'NONE', *, *, #12732, .F. ) ;
#7140=DIRECTION ( 'NONE',  ( -1.000000000000000000, 0.000000000000000000, 0.000000000000000000 ) ) ;
#7155=VERTEX_POINT ( 'NONE', #1420 ) ;
#7156=EDGE_CURVE ( 'NONE', #6805, #5852, #11869, .T. ) ;
#7157=ORIENTED_EDGE ( 'NONE', *, *, #12024, .T. ) ;
#7160=CARTESIAN_POINT ( 'NONE',  ( -6.532899837730830939, 4.269496439496346535E-15, -5.432899837730820636 ) ) ;
#7166=CARTESIAN_POINT ( 'NONE',  ( 5.170224855064536662, -2.788471980053871757, -4.589066185948674104 ) ) ;
#7170=B_SPLINE_CURVE_WITH_KNOTS ( 'NONE', 3,
 ( #12046, #783, #7357, #11832, #6255, #10730, #14390, #10056, #11220, #10189 ),
 .UNSPECIFIED., .F., .F.,
 ( 4, 2, 2, 2, 4 ),
 ( 0.000000000000000000, 0.001528561485809836482, 0.003057122971619672964, 0.004585684457429509663, 0.006114245943239347662 ),
 .UNSPECIFIED. ) ;
#7173=B_SPLINE_CURVE_WITH_KNOTS ( 'NONE', 3,
 ( #14382, #8867, #9979, #7616, #2157 ),
 .UNSPECIFIED., .F., .F.,
 ( 4, 1, 4 ),
 ( 0.000000000000000000, 0.002886751345948135056, 0.005773502691896270113 ),
 .UNSPECIFIED. ) ;
#7178=AXIS2_PLACEMENT_3D ( 'NONE', #10598, #11611, #10520 ) ;
#7208=EDGE_CURVE ( 'NONE', #32, #14260, #13987, .T. ) ;
#7226=DIRECTION ( 'NONE',  ( 0.8660254037844373753, 0.5000000000000022204, 2.348866325434637045E-33 ) ) ;
#7234=ORIENTED_EDGE ( 'NONE', *, *, #3611, .T. ) ;
#7238=CIRCLE ( 'NONE', #2580, 5.000000000000000888 ) ;
#7246=CARTESIAN_POINT ( 'NONE',  ( -1.598077599629839529, -4.850852159564174038, -4.271474537231504165 ) ) ;
#7247=ORIENTED_EDGE ( 'NONE', *, *, #13289, .T. ) ;
#7265=CARTESIAN_POINT ( 'NONE',  ( -6.726859516510133474, 3.469446951953614189E-15, -4.900000000000015454 ) ) ;
#7282=CARTESIAN_POINT ( 'NONE',  ( 3.000000000000000888, 3.836840991697820422E-15, -5.974599999999997024 ) ) ;
#7291=CIRCLE ( 'NONE', #8218, 5.000000000000000888 ) ;
#7293=ORIENTED_EDGE ( 'NONE', *, *, #580, .F. ) ;
#7299=ORIENTED_EDGE ( 'NONE', *, *, #9678, .T. ) ;
#7328=CARTESIAN_POINT ( 'NONE',  ( -1.582370436564039196, -4.859920694388334184, -4.019399823476004663 ) ) ;
#7337=DIRECTION ( 'NONE',  ( 0.000000000000000000, 8.482162385747133845E-47, -1.000000000000000000 ) ) ;
#7349=VERTEX_POINT ( 'NONE', #3921 ) ;
#7357=CARTESIAN_POINT ( 'NONE',  ( -0.8665032349992132232, -5.555903485205178960, -4.490643565754968591 ) ) ;
#7385=CARTESIAN_POINT ( 'NONE',  ( 2.176667689905607883, 4.790324513057876210, -4.357749648769117634 ) ) ;
#7390=EDGE_CURVE ( 'NONE', #12268, #10194, #13169, .T. ) ;
#7393=CARTESIAN_POINT ( 'NONE',  ( -0.03111943836866669019, -6.084399642271201003, -4.666192694417985010 ) ) ;
#7401=ORIENTED_EDGE ( 'NONE', *, *, #7000, .F. ) ;
#7402=CARTESIAN_POINT ( 'NONE',  ( -5.244800587397357106, -2.026986389275633016, -4.490560292650636498 ) ) ;
#7431=CARTESIAN_POINT ( 'NONE',  ( 2.714587707229028535, -4.206234748388760991, -2.116820038483221662E-14 ) ) ;
#7444=CARTESIAN_POINT ( 'NONE',  ( -5.594483210025202879E-14, -5.773502691896268857, -0.5999999999999894307 ) ) ;
#7451=EDGE_CURVE ( 'NONE', #3061, #3492, #7173, .T. ) ;
#7456=PRESENTATION_STYLE_ASSIGNMENT (( #10903 ) ) ;
#7463=UNCERTAINTY_MEASURE_WITH_UNIT (LENGTH_MEASURE( 1.000000000000000082E-05 ), #12019, 'distance_accuracy_value', 'NONE');
#7468=CARTESIAN_POINT ( 'NONE',  ( -5.253368672218639013, -3.033033817057793957, -4.659491423763650886 ) ) ;
#7499=EDGE_LOOP ( 'NONE', ( #1434, #13339, #9382, #1256 ) ) ;
#7538=CARTESIAN_POINT ( 'NONE',  ( -5.284804376168110274, -3.015249596956827816, -4.666192694417973463 ) ) ;
#7554=CYLINDRICAL_SURFACE ( 'NONE', #4045, 2.500000000000000444 ) ;
#7560=ORIENTED_EDGE ( 'NONE', *, *, #8716, .F. ) ;
#7595=CARTESIAN_POINT ( 'NONE',  ( 5.000000000000000888, 2.424500739214346723, -0.4207179063848164313 ) ) ;
#7616=CARTESIAN_POINT ( 'NONE',  ( 5.000000000000002665, 1.924500897298742963, -4.118275046351175916 ) ) ;
#7625=DIRECTION ( 'NONE',  ( 1.000000000000000000, 0.000000000000000000, 0.000000000000000000 ) ) ;
#7660=MECHANICAL_DESIGN_GEOMETRIC_PRESENTATION_REPRESENTATION('',(#14006),#4202);
#7665=SURFACE_STYLE_USAGE ( .BOTH. , #12367 ) ;
#7673=CARTESIAN_POINT ( 'NONE',  ( 0.000000000000000000, 0.000000000000000000, -0.3501037691048258793 ) ) ;
#7681=EDGE_LOOP ( 'NONE', ( #11198, #13544, #8051, #13200, #11094 ) ) ;
#7685=B_SPLINE_CURVE_WITH_KNOTS ( 'NONE', 3,
 ( #7468, #12920, #7402, #8514, #6167, #693 ),
 .UNSPECIFIED., .F., .F.,
 ( 4, 2, 4 ),
 ( 0.000000000000000000, 0.001529397995383623013, 0.003058795990767246026 ),
 .UNSPECIFIED. ) ;
#7696=ORIENTED_EDGE ( 'NONE', *, *, #11713, .F. ) ;
#7706=ORIENTED_EDGE ( 'NONE', *, *, #3890, .F. ) ;
#7750=CARTESIAN_POINT ( 'NONE',  ( -0.8653900595644484772, 5.556556492855584395, -4.490801088233111749 ) ) ;
#7752=CARTESIAN_POINT ( 'NONE',  ( 5.000000000000000000, -2.886751345948148639, -4.284345921091780696 ) ) ;
#7775=ORIENTED_EDGE ( 'NONE', *, *, #10209, .T. ) ;
#7780=CARTESIAN_POINT ( 'NONE',  ( -0.8333333333333305948, 5.292377467571583338, -4.118275046351175028 ) ) ;
#7799=ORIENTED_EDGE ( 'NONE', *, *, #1844, .F. ) ;
#7806=DIRECTION ( 'NONE',  ( 0.000000000000000000, 8.482162385747133845E-47, -1.000000000000000000 ) ) ;
#7812=CARTESIAN_POINT ( 'NONE',  ( -5.253368672218636348, 3.033033817057773085, -4.659491423763650886 ) ) ;
#7822=CARTESIAN_POINT ( 'NONE',  ( 5.000000000000001776, 1.231908430319626602, -0.1119772403577116160 ) ) ;
#7847=ADVANCED_FACE ( 'NONE', ( #10629 ), #12828, .F. ) ;
#7853=AXIS2_PLACEMENT_3D ( 'NONE', #1632, #8575, #1787 ) ;
#7859=DIRECTION ( 'NONE',  ( 1.000000000000000000, 0.000000000000000000, 0.000000000000000000 ) ) ;
#7891=CARTESIAN_POINT ( 'NONE',  ( 4.378301941662550156, -3.528365556573312301, -4.490643565754961486 ) ) ;
#7924=CARTESIAN_POINT ( 'NONE',  ( -3.352586340487487160, -3.837886065734366525, -0.05822226285684464070 ) ) ;
#7929=DIRECTION ( 'NONE',  ( 1.000000000000000000, 0.000000000000000000, 0.000000000000000000 ) ) ;
#7938=ORIENTED_EDGE ( 'NONE', *, *, #12246, .T. ) ;
#7939=AXIS2_PLACEMENT_3D ( 'NONE', #4666, #12621, #8229 ) ;
#7944=CARTESIAN_POINT ( 'NONE',  ( 5.000000000000001776, -2.092693589761094763, -4.400105005940151415 ) ) ;
#7964=DIRECTION ( 'NONE',  ( -0.8191520442889913545, 1.003171929053524254E-16, 0.5735764363510468256 ) ) ;
#7967=ORIENTED_EDGE ( 'NONE', *, *, #10476, .F. ) ;
#8022=CARTESIAN_POINT ( 'NONE',  ( 1.647413659512545037, -4.822367972110058965, -0.05822226285685259267 ) ) ;
#8034=CARTESIAN_POINT ( 'NONE',  ( -5.000000000000000888, -2.068736481089864743, -4.395493724530259882 ) ) ;
#8051=ORIENTED_EDGE ( 'NONE', *, *, #3210, .T. ) ;
#8063=CARTESIAN_POINT ( 'NONE',  ( 0.2117491801717979183, 5.895756138069145003, -4.327903350935045523 ) ) ;
#8073=ORIENTED_EDGE ( 'NONE', *, *, #5913, .T. ) ;
#8074=FACE_OUTER_BOUND ( 'NONE', #10719, .T. ) ;
#8100=CARTESIAN_POINT ( 'NONE',  ( -5.000000000000000000, 2.119023573395804050, -4.142091658825685307 ) ) ;
#8111=AXIS2_PLACEMENT_3D ( 'NONE', #8832, #6559, #3371 ) ;
#8113=EDGE_CURVE ( 'NONE', #6870, #10194, #11631, .T. ) ;
#8114=CARTESIAN_POINT ( 'NONE',  ( 6.202806007537712125E-14, -5.987311224403027765, -4.630826434870603414 ) ) ;
#8136=EDGE_CURVE ( 'NONE', #10931, #4994, #9462, .T. ) ;
#8172=ORIENTED_EDGE ( 'NONE', *, *, #928, .T. ) ;
#8175=CARTESIAN_POINT ( 'NONE',  ( -5.000000000000000888, -1.027005139385383847, -4.269881284526090504 ) ) ;
#8212=CARTESIAN_POINT ( 'NONE',  ( 4.296971609537894032, 3.292644976429773163, -4.396693167834091476 ) ) ;
#8218=AXIS2_PLACEMENT_3D ( 'NONE', #8423, #881, #5059 ) ;
#8229=DIRECTION ( 'NONE',  ( 1.000000000000000000, 0.000000000000000000, 0.000000000000000000 ) ) ;
#8262=EDGE_CURVE ( 'NONE', #9023, #13190, #13686, .T. ) ;
#8270=CARTESIAN_POINT ( 'NONE',  ( -5.170224855064537550, -2.788471980053867760, -4.589066185948674104 ) ) ;
#8286=ORIENTED_EDGE ( 'NONE', *, *, #12246, .F. ) ;
#8292=DIRECTION ( 'NONE',  ( -1.000000000000000000, 0.000000000000000000, 0.000000000000000000 ) ) ;
#8307=DIRECTION ( 'NONE',  ( 1.000000000000000000, 0.000000000000000000, 0.000000000000000000 ) ) ;
#8308=CARTESIAN_POINT ( 'NONE',  ( -1.432312439535613269, -4.946556719366752120, -0.1121614189353486168 ) ) ;
#8311=ORIENTED_EDGE ( 'NONE', *, *, #7000, .T. ) ;
#8313=ORIENTED_EDGE ( 'NONE', *, *, #13289, .F. ) ;
#8321=DIRECTION ( 'NONE',  ( 0.000000000000000000, 8.482162385747133845E-47, -1.000000000000000000 ) ) ;
#8333=VERTEX_POINT ( 'NONE', #11093 ) ;
#8373=CONICAL_SURFACE ( 'NONE', #13971, 5.000000000000000888, 0.9110539511682884672 ) ;
#8379=ORIENTED_EDGE ( 'NONE', *, *, #10209, .F. ) ;
#8403=CARTESIAN_POINT ( 'NONE',  ( -1.752700365193367750E-15, -5.773502691896300831, -6.000000000000005329 ) ) ;
#8420=CARTESIAN_POINT ( 'NONE',  ( 4.400655246570930323, -3.515428273946614723, -4.476900509771775560 ) ) ;
#8423=CARTESIAN_POINT ( 'NONE',  ( 0.000000000000000000, 0.000000000000000000, 0.000000000000000000 ) ) ;
#8438=ADVANCED_FACE ( 'NONE', ( #1503 ), #13969, .T. ) ;
#8440=CARTESIAN_POINT ( 'NONE',  ( 3.401922400370811506, 3.809401878279405462, -4.271474537231044089 ) ) ;
#8446=VERTEX_POINT ( 'NONE', #3703 ) ;
#8466=VECTOR ( 'NONE', #8907, 1000.000000000000000 ) ;
#8470=CARTESIAN_POINT ( 'NONE',  ( 4.598786737361985288, -3.118391931134659956, -0.4203182062997378177 ) ) ;
#8486=DIRECTION ( 'NONE',  ( 1.000000000000000000, 0.000000000000000000, 0.000000000000000000 ) ) ;
#8501=CARTESIAN_POINT ( 'NONE',  ( 1.582370436564208838, -4.859920694388245366, -4.019399823475544586 ) ) ;
#8502=CARTESIAN_POINT ( 'NONE',  ( -3.514986608502201904, -4.017641317387708355, -4.357689166958490290 ) ) ;
#8514=CARTESIAN_POINT ( 'NONE',  ( -5.238704763094644612, -1.015773027556925223, -4.385839086323478853 ) ) ;
#8541=ADVANCED_FACE ( 'NONE', ( #9700 ), #9753, .T. ) ;
#8547=EDGE_LOOP ( 'NONE', ( #1850, #5601, #1892, #5905 ) ) ;
#8568=CARTESIAN_POINT ( 'NONE',  ( 3.417629563435787610, -3.800333343456214319, -4.019399823475544586 ) ) ;
#8574=CARTESIAN_POINT ( 'NONE',  ( 5.244800587397359770, 2.026986389275614364, -4.490560292650632945 ) ) ;
#8575=DIRECTION ( 'NONE',  ( -1.000000000000000000, 0.000000000000000000, 0.000000000000000000 ) ) ;
#8589=CARTESIAN_POINT ( 'NONE',  ( 5.000000000000005329, -2.886751345948144643, -4.369522543421425098 ) ) ;
#8639=FACE_OUTER_BOUND ( 'NONE', #5745, .T. ) ;
#8643=CARTESIAN_POINT ( 'NONE',  ( 4.451998719175967729E-15, 5.807445019730661961, -4.451004066889661104 ) ) ;
#8664=CARTESIAN_POINT ( 'NONE',  ( -3.081487911019577365E-30, 3.469446951953614189E-15, -5.432899837730820636 ) ) ;
#8670=CARTESIAN_POINT ( 'NONE',  ( -2.500000000000011990, 4.330127018922186544, 0.000000000000000000 ) ) ;
#8674=CARTESIAN_POINT ( 'NONE',  ( -3.081487911019577365E-30, 3.469446951953614189E-15, -5.974599999999997024 ) ) ;
#8677=ORIENTED_EDGE ( 'NONE', *, *, #580, .T. ) ;
#8678=CARTESIAN_POINT ( 'NONE',  ( 0.000000000000000000, 0.000000000000000000, 0.000000000000000000 ) ) ;
#8681=( GEOMETRIC_REPRESENTATION_CONTEXT ( 3 ) GLOBAL_UNCERTAINTY_ASSIGNED_CONTEXT ( ( #7463 ) ) GLOBAL_UNIT_ASSIGNED_CONTEXT ( ( #12019, #4201, #949 ) ) REPRESENTATION_CONTEXT ( 'NONE', 'WORKASPACE' ) );
#8688=CARTESIAN_POINT ( 'NONE',  ( 4.185558440016316162, 3.356969399843931612, -0.2680587191991122276 ) ) ;
#8716=EDGE_CURVE ( 'NONE', #7073, #32, #3367, .T. ) ;
#8735=B_SPLINE_CURVE_WITH_KNOTS ( 'NONE', 3,
 ( #9381, #240, #12669, #3905, #1625, #4710 ),
 .UNSPECIFIED., .F., .F.,
 ( 4, 2, 4 ),
 ( -3.988673288085428471E-06, 0.0002483701411510698723, 0.0005007289555902250935 ),
 .UNSPECIFIED. ) ;
#8745=DIRECTION ( 'NONE',  ( 0.000000000000000000, 8.482162385747133845E-47, -1.000000000000000000 ) ) ;
#8756=EDGE_CURVE ( 'NONE', #981, #1738, #3229, .T. ) ;
#8763=PLANE ( 'NONE',  #8111 ) ;
#8769=EDGE_CURVE ( 'NONE', #13012, #3061, #3033, .T. ) ;
#8770=ORIENTED_EDGE ( 'NONE', *, *, #206, .T. ) ;
#8776=CARTESIAN_POINT ( 'NONE',  ( -5.000000000000000000, 0.2466074518009251093, 6.437450399132684549E-16 ) ) ;
#8781=PLANE ( 'NONE',  #6110 ) ;
#8800=EDGE_LOOP ( 'NONE', ( #13504, #4683, #10409, #7401 ) ) ;
#8805=CARTESIAN_POINT ( 'NONE',  ( -2.499999999999999556, 4.330127018922202531, -3.920524600599842202 ) ) ;
#8817=DIRECTION ( 'NONE',  ( 0.000000000000000000, -8.482162385747133845E-47, 1.000000000000000000 ) ) ;
#8818=CARTESIAN_POINT ( 'NONE',  ( -2.931639317407896073, 4.080919942823921787, -0.01465562841807914810 ) ) ;
#8832=CARTESIAN_POINT ( 'NONE',  ( 2.602085213965210642E-15, 5.773502691896274186, -6.000000000000005329 ) ) ;
#8844=CARTESIAN_POINT ( 'NONE',  ( 2.179555516819076999, -4.788648424347465848, -4.357628883416072796 ) ) ;
#8863=AXIS2_PLACEMENT_3D ( 'NONE', #7160, #4130, #9595 ) ;
#8866=ORIENTED_EDGE ( 'NONE', *, *, #601, .T. ) ;
#8867=CARTESIAN_POINT ( 'NONE',  ( 4.999999999999999112, -1.924500897298769608, -4.118275046351174140 ) ) ;
#8884=CARTESIAN_POINT ( 'NONE',  ( -1.598077599628788370, 4.850852159564692734, -4.271474537231044977 ) ) ;
#8887=CARTESIAN_POINT ( 'NONE',  ( -3.357433326862111489, 3.835087656846199788, -0.07080520455421618342 ) ) ;
#8907=DIRECTION ( 'NONE',  ( 0.000000000000000000, -8.482162385747133845E-47, 1.000000000000000000 ) ) ;
#8920=B_SPLINE_CURVE_WITH_KNOTS ( 'NONE', 3,
 ( #11920, #5321, #9784, #8688, #3148, #11168 ),
 .UNSPECIFIED., .F., .F.,
 ( 4, 2, 4 ),
 ( 0.002950759650825679654, 0.004429055062152274097, 0.005907350473478867672 ),
 .UNSPECIFIED. ) ;
#8938=FACE_OUTER_BOUND ( 'NONE', #6318, .T. ) ;
#8941=VERTEX_POINT ( 'NONE', #13092 ) ;
#8963=LINE ( 'NONE', #13232, #11651 ) ;
#8967=VERTEX_POINT ( 'NONE', #4397 ) ;
#8973=CARTESIAN_POINT ( 'NONE',  ( 0.000000000000000000, 0.000000000000000000, -0.3501037691048258793 ) ) ;
#8976=ADVANCED_FACE ( 'NONE', ( #860, #14411 ), #8763, .T. ) ;
#8979=CARTESIAN_POINT ( 'NONE',  ( -5.594483210025202879E-14, -5.773502691896268857, -0.5999999999999894307 ) ) ;
#8989=CARTESIAN_POINT ( 'NONE',  ( -5.000000000000000000, 3.082653260002450768, -4.588940887454125317 ) ) ;
#9012=ORIENTED_EDGE ( 'NONE', *, *, #5664, .F. ) ;
#9023=VERTEX_POINT ( 'NONE', #3289 ) ;
#9037=CARTESIAN_POINT ( 'NONE',  ( 5.000000000000001776, 2.094482489769011302, -4.137545075662903749 ) ) ;
#9048=ORIENTED_EDGE ( 'NONE', *, *, #10476, .T. ) ;
#9056=CARTESIAN_POINT ( 'NONE',  ( -1.532072935877364915E-15, -6.066067634115591467, -4.659491423763650886 ) ) ;
#9084=ADVANCED_FACE ( 'NONE', ( #5472 ), #11871, .T. ) ;
#9099=ORIENTED_EDGE ( 'NONE', *, *, #928, .F. ) ;
#9108=CARTESIAN_POINT ( 'NONE',  ( 5.244936800657701070, -2.071448270550554138, -4.480299463185753339 ) ) ;
#9114=CARTESIAN_POINT ( 'NONE',  ( -3.081487911019577365E-30, 3.469446951953614189E-15, -5.624496230895170257 ) ) ;
#9123=ORIENTED_EDGE ( 'NONE', *, *, #2501, .F. ) ;
#9134=EDGE_CURVE ( 'NONE', #32, #10813, #13397, .T. ) ;
#9136=B_SPLINE_CURVE_WITH_KNOTS ( 'NONE', 3,
 ( #10887, #12066, #13105, #6480, #4254, #11998 ),
 .UNSPECIFIED., .F., .F.,
 ( 4, 2, 4 ),
 ( 0.003058795990767210031, 0.004586520967003277979, 0.006114245943239346795 ),
 .UNSPECIFIED. ) ;
#9140=CARTESIAN_POINT ( 'NONE',  ( 2.500000000000011546, -4.330127018922186544, 0.000000000000000000 ) ) ;
#9177=EDGE_LOOP ( 'NONE', ( #8286, #11091, #13236, #13999 ) ) ;
#9185=CARTESIAN_POINT ( 'NONE',  ( 5.000000000000000888, -3.082649547295097658, -4.588940179250877271 ) ) ;
#9195=CARTESIAN_POINT ( 'NONE',  ( 5.000000000000000888, 0.000000000000000000, 0.000000000000000000 ) ) ;
#9199=ORIENTED_EDGE ( 'NONE', *, *, #7156, .F. ) ;
#9242=CARTESIAN_POINT ( 'NONE',  ( 3.514986608502523868, 4.017641317387379729, -4.357689166958453875 ) ) ;
#9270=EDGE_LOOP ( 'NONE', ( #6407, #2425, #11756 ) ) ;
#9282=CARTESIAN_POINT ( 'NONE',  ( 5.253368672218638125, 3.033033817057769532, -4.659491423763650886 ) ) ;
#9287=FACE_BOUND ( 'NONE', #5697, .T. ) ;
#9295=AXIS2_PLACEMENT_3D ( 'NONE', #1585, #4958, #1520 ) ;
#9311=CARTESIAN_POINT ( 'NONE',  ( 3.370256023960729782E-15, 5.773502691896274186, -6.000000000000005329 ) ) ;
#9341=CARTESIAN_POINT ( 'NONE',  ( 5.000000000000000000, -2.886751345948148639, -4.284345921091780696 ) ) ;
#9381=CARTESIAN_POINT ( 'NONE',  ( -5.253368672218639013, -3.033033817057793957, -4.659491423763650886 ) ) ;
#9382=ORIENTED_EDGE ( 'NONE', *, *, #11245, .F. ) ;
#9406=ORIENTED_EDGE ( 'NONE', *, *, #6043, .F. ) ;
#9415=DIRECTION ( 'NONE',  ( -1.000000000000000000, 0.000000000000000000, 0.000000000000000000 ) ) ;
#9418=CARTESIAN_POINT ( 'NONE',  ( 0.000000000000000000, 0.000000000000000000, 0.000000000000000000 ) ) ;
#9424=CARTESIAN_POINT ( 'NONE',  ( -5.594483210025202879E-14, -5.773502691896268857, -0.5999999999999894307 ) ) ;
#9436=CARTESIAN_POINT ( 'NONE',  ( -1.752700365193367750E-15, -5.773502691896300831, -6.000000000000005329 ) ) ;
#9462=B_SPLINE_CURVE_WITH_KNOTS ( 'NONE', 3,
 ( #9424, #3873, #583, #8308, #12785, #13425, #12867, #9779 ),
 .UNSPECIFIED., .F., .F.,
 ( 4, 2, 2, 4 ),
 ( 2.451332857528375667E-07, 0.001475502392055722152, 0.002213131021440706107, 0.002950759650825690496 ),
 .UNSPECIFIED. ) ;
#9486=ORIENTED_EDGE ( 'NONE', *, *, #2194, .T. ) ;
#9542=CARTESIAN_POINT ( 'NONE',  ( 2.500000000000000444, 3.469446951953614189E-15, -5.624496230895170257 ) ) ;
#9546=CARTESIAN_POINT ( 'NONE',  ( 4.400655246570535972, 3.515428273946802129, -4.476900509771682302 ) ) ;
#9552=ADVANCED_FACE ( 'NONE', ( #5247 ), #1982, .F. ) ;
#9595=DIRECTION ( 'NONE',  ( -1.000000000000000000, 1.224646799147352714E-16, 0.000000000000000000 ) ) ;
#9598=EDGE_CURVE ( 'NONE', #6152, #3422, #10135, .T. ) ;
#9603=ORIENTED_EDGE ( 'NONE', *, *, #6981, .F. ) ;
#9605=CARTESIAN_POINT ( 'NONE',  ( -5.253368672218636348, 3.033033817057773085, -4.659491423763650886 ) ) ;
#9614=ORIENTED_EDGE ( 'NONE', *, *, #4501, .F. ) ;
#9631=ORIENTED_EDGE ( 'NONE', *, *, #3611, .F. ) ;
#9649=ORIENTED_EDGE ( 'NONE', *, *, #7208, .T. ) ;
#9658=PRODUCT_CONTEXT ( 'NONE', #4388, 'mechanical' ) ;
#9663=CARTESIAN_POINT ( 'NONE',  ( 3.057313426867670714, 4.281874658697562452, -4.357628883416062138 ) ) ;
#9674=PRODUCT_DEFINITION_FORMATION_WITH_SPECIFIED_SOURCE ( 'ANY', '', #2643, .NOT_KNOWN. ) ;
#9678=EDGE_CURVE ( 'NONE', #3061, #9023, #2307, .T. ) ;
#9685=CARTESIAN_POINT ( 'NONE',  ( -5.029394918168159201, 2.903722509865322543, -4.451004066889655775 ) ) ;
#9686=CARTESIAN_POINT ( 'NONE',  ( 5.248984340851196251, 2.531668808681887928, -4.566868479993924090 ) ) ;
#9700=FACE_OUTER_BOUND ( 'NONE', #14369, .T. ) ;
#9702=CARTESIAN_POINT ( 'NONE',  ( 5.000000000000000000, -2.886751345948148639, -4.284345921091780696 ) ) ;
#9708=DIRECTION ( 'NONE',  ( 0.000000000000000000, -8.482162385747133845E-47, 1.000000000000000000 ) ) ;
#9745=CONICAL_SURFACE ( 'NONE', #5756, 5.000000000000000888, 0.9110539511682884672 ) ;
#9749=CARTESIAN_POINT ( 'NONE',  ( -5.000000000000001776, -2.886751345948141534, -6.000000000000005329 ) ) ;
#9753=TOROIDAL_SURFACE ( 'NONE', #4619, 6.532899837730830939, 0.5671001622691684840 ) ;
#9779=CARTESIAN_POINT ( 'NONE',  ( -2.500000000000016875, -4.330127018922186544, 0.000000000000000000 ) ) ;
#9784=CARTESIAN_POINT ( 'NONE',  ( 3.352586340487478278, 3.837886065734358532, -0.05822226285683582137 ) ) ;
#9791=DIRECTION ( 'NONE',  ( -1.000000000000000000, 0.000000000000000000, 0.000000000000000000 ) ) ;
#9800=CONICAL_SURFACE ( 'NONE', #13560, 5.000000000000000888, 0.9110539511682884672 ) ;
#9806=DIRECTION ( 'NONE',  ( 1.000000000000000000, 0.000000000000000000, 0.000000000000000000 ) ) ;
#9831=VERTEX_POINT ( 'NONE', #2825 ) ;
#9843=CONICAL_SURFACE ( 'NONE', #10311, 5.000000000000000888, 0.9110539511682884672 ) ;
#9846=EDGE_CURVE ( 'NONE', #13192, #7349, #12841, .T. ) ;
#9849=CARTESIAN_POINT ( 'NONE',  ( -4.296971609536595516, 3.292644976429713655, -4.396693167835552529 ) ) ;
#9885=CARTESIAN_POINT ( 'NONE',  ( -5.253368672218636348, 3.033033817057773085, -4.659491423763650886 ) ) ;
#9889=CARTESIAN_POINT ( 'NONE',  ( -2.450000000000000622, 3.000384657911016356E-16, -0.3851141460153306717 ) ) ;
#9894=CARTESIAN_POINT ( 'NONE',  ( -5.000000000000001776, -2.886751345948152192, -4.284345921091780696 ) ) ;
#9979=CARTESIAN_POINT ( 'NONE',  ( 5.000000000000001776, -1.387778780781445676E-14, -3.920524600599840426 ) ) ;
#10056=CARTESIAN_POINT ( 'NONE',  ( -4.379424050594064255, -3.527728022193145296, -4.490801088233112637 ) ) ;
#10060=CARTESIAN_POINT ( 'NONE',  ( 5.000000000000000000, -2.886751345948148639, -6.000000000000005329 ) ) ;
#10075=CARTESIAN_POINT ( 'NONE',  ( 5.000000000000001776, 1.044497431481508531, -4.017831869288535529 ) ) ;
#10115=ORIENTED_EDGE ( 'NONE', *, *, #12539, .T. ) ;
#10134=B_SPLINE_CURVE_WITH_KNOTS ( 'NONE', 3,
 ( #1301, #13475, #7891, #4412, #5688, #8844, #2337, #148, #4615, #9056 ),
 .UNSPECIFIED., .F., .F.,
 ( 4, 2, 2, 2, 4 ),
 ( 0.000000000000000000, 0.001528561485809835615, 0.003057122971619672530, 0.004585684457429509663, 0.006114245943239346795 ),
 .UNSPECIFIED. ) ;
#10135=LINE ( 'NONE', #6757, #13065 ) ;
#10145=B_SPLINE_CURVE_WITH_KNOTS ( 'NONE', 3,
 ( #8670, #13158, #13442, #5581, #5781, #38 ),
 .UNSPECIFIED., .F., .F.,
 ( 4, 2, 4 ),
 ( 0.002950759650825642358, 0.004429055062152263689, 0.005907350473478885887 ),
 .UNSPECIFIED. ) ;
#10178=DIRECTION ( 'NONE',  ( -1.000000000000000000, 0.000000000000000000, 0.000000000000000000 ) ) ;
#10187=ADVANCED_FACE ( 'NONE', ( #14067 ), #13986, .F. ) ;
#10189=CARTESIAN_POINT ( 'NONE',  ( -5.253368672218639013, -3.033033817057793957, -4.659491423763650886 ) ) ;
#10194=VERTEX_POINT ( 'NONE', #519 ) ;
#10195=CARTESIAN_POINT ( 'NONE',  ( 0.03111943836866626692, 6.084399642271180575, -4.666192694417975240 ) ) ;
#10209=EDGE_CURVE ( 'NONE', #13012, #10931, #3888, .T. ) ;
#10231=( LENGTH_UNIT ( ) NAMED_UNIT ( * ) SI_UNIT ( .MILLI., .METRE. ) );
#10233=CARTESIAN_POINT ( 'NONE',  ( -5.000000000000000000, -3.131510016925063589, -4.327949577589330410 ) ) ;
#10243=VERTEX_POINT ( 'NONE', #6488 ) ;
#10265=DIRECTION ( 'NONE',  ( 0.000000000000000000, -8.482162385747133845E-47, 1.000000000000000000 ) ) ;
#10311=AXIS2_PLACEMENT_3D ( 'NONE', #13709, #3676, #10178 ) ;
#10332=VERTEX_POINT ( 'NONE', #7812 ) ;
#10350=ORIENTED_EDGE ( 'NONE', *, *, #4631, .F. ) ;
#10353=EDGE_CURVE ( 'NONE', #13190, #10931, #632, .T. ) ;
#10358=DIRECTION ( 'NONE',  ( -1.000000000000000000, 0.000000000000000000, 0.000000000000000000 ) ) ;
#10367=FACE_OUTER_BOUND ( 'NONE', #12957, .T. ) ;
#10368=ORIENTED_EDGE ( 'NONE', *, *, #2487, .T. ) ;
#10373=DIRECTION ( 'NONE',  ( -0.000000000000000000, -8.482162385747133845E-47, 1.000000000000000000 ) ) ;
#10386=CARTESIAN_POINT ( 'NONE',  ( -5.253687112945022442, -3.069398100742061875, -4.666238921072260126 ) ) ;
#10394=DIRECTION ( 'NONE',  ( 0.000000000000000000, 8.482162385747133845E-47, -1.000000000000000000 ) ) ;
#10409=ORIENTED_EDGE ( 'NONE', *, *, #8756, .T. ) ;
#10418=DIRECTION ( 'NONE',  ( 1.000000000000000000, 0.000000000000000000, 0.000000000000000000 ) ) ;
#10428=EDGE_CURVE ( 'NONE', #6152, #6044, #5831, .T. ) ;
#10437=DIRECTION ( 'NONE',  ( 0.000000000000000000, -8.482162385747133845E-47, 1.000000000000000000 ) ) ;
#10476=EDGE_CURVE ( 'NONE', #11372, #8967, #13466, .T. ) ;
#10490=CARTESIAN_POINT ( 'NONE',  ( 5.170224855064536662, 2.788471980053847332, -4.589066185948671439 ) ) ;
#10494=B_SPLINE_CURVE_WITH_KNOTS ( 'NONE', 3,
 ( #6006, #4926, #3692, #394, #2588, #7035 ),
 .UNSPECIFIED., .F., .F.,
 ( 4, 2, 4 ),
 ( 0.003058795990767246026, 0.004586520967003294459, 0.006114245943239343326 ),
 .UNSPECIFIED. ) ;
#10512=DIRECTION ( 'NONE',  ( 1.000000000000000000, 0.000000000000000000, 0.000000000000000000 ) ) ;
#10520=DIRECTION ( 'NONE',  ( 1.000000000000000000, 0.000000000000000000, 0.000000000000000000 ) ) ;
#10522=CONICAL_SURFACE ( 'NONE', #2118, 3.000000000000000888, 0.9599310885968798113 ) ;
#10530=PLANE ( 'NONE',  #1868 ) ;
#10562=ORIENTED_EDGE ( 'NONE', *, *, #7451, .T. ) ;
#10566=CARTESIAN_POINT ( 'NONE',  ( -0.2117491801717900912, 5.895756138069147667, -4.327903350935046412 ) ) ;
#10585=CARTESIAN_POINT ( 'NONE',  ( 5.000000000000001776, 2.886751345948127767, -6.000000000000005329 ) ) ;
#10594=DIRECTION ( 'NONE',  ( -1.000000000000000000, 0.000000000000000000, 0.000000000000000000 ) ) ;
#10598=CARTESIAN_POINT ( 'NONE',  ( 0.000000000000000000, 0.000000000000000000, 0.000000000000000000 ) ) ;
#10616=LINE ( 'NONE', #5980, #6809 ) ;
#10629=FACE_OUTER_BOUND ( 'NONE', #4132, .T. ) ;
#10635=PLANE ( 'NONE',  #6550 ) ;
#10638=DIRECTION ( 'NONE',  ( 0.000000000000000000, -8.482162385747133845E-47, 1.000000000000000000 ) ) ;
#10644=CARTESIAN_POINT ( 'NONE',  ( 5.284804376168111162, 3.015249596956805611, -4.666192694417969022 ) ) ;
#10647=ORIENTED_EDGE ( 'NONE', *, *, #601, .F. ) ;
#10671=CARTESIAN_POINT ( 'NONE',  ( 3.357433326862117262, -3.835087656846223769, -0.07080520455423312820 ) ) ;
#10698=CARTESIAN_POINT ( 'NONE',  ( 0.7030283904627421254, -5.367609061415554272, -4.396693167834692773 ) ) ;
#10700=CARTESIAN_POINT ( 'NONE',  ( -0.7030283904623975122, -5.367609061414145621, -4.396693167834326843 ) ) ;
#10701=EDGE_LOOP ( 'NONE', ( #11000, #13941, #3534, #11952 ) ) ;
#10719=EDGE_LOOP ( 'NONE', ( #11693, #9048, #4662, #11820, #4567, #3575, #10996 ) ) ;
#10730=CARTESIAN_POINT ( 'NONE',  ( -3.057313426867662720, -4.281874658697580216, -4.357628883416065690 ) ) ;
#10734=CARTESIAN_POINT ( 'NONE',  ( 5.000000000000001776, 2.886751345948152192, -0.5999999999999894307 ) ) ;
#10744=ORIENTED_EDGE ( 'NONE', *, *, #8716, .T. ) ;
#10753=DIRECTION ( 'NONE',  ( 1.000000000000000000, 0.000000000000000000, 0.000000000000000000 ) ) ;
#10756=ADVANCED_FACE ( 'NONE', ( #8639 ), #11698, .F. ) ;
#10759=CARTESIAN_POINT ( 'NONE',  ( 0.8665032349992187743, 5.555903485205162085, -4.490643565754959710 ) ) ;
#10768=( NAMED_UNIT ( * ) PLANE_ANGLE_UNIT ( ) SI_UNIT ( $, .RADIAN. ) );
#10781=CARTESIAN_POINT ( 'NONE',  ( 5.253368672218638125, 3.033033817057769532, -4.659491423763650886 ) ) ;
#10791=CARTESIAN_POINT ( 'NONE',  ( 0.4012132626380313649, 5.541862106709766422, -0.4203182062997399826 ) ) ;
#10813=VERTEX_POINT ( 'NONE', #2482 ) ;
#10828=CARTESIAN_POINT ( 'NONE',  ( -5.000000000000000000, 2.886751345948127767, -6.000000000000005329 ) ) ;
#10839=AXIS2_PLACEMENT_3D ( 'NONE', #3574, #4735, #5799 ) ;
#10887=CARTESIAN_POINT ( 'NONE',  ( 5.236872748402767286, 8.765285303662936917E-14, -4.357689166958464533 ) ) ;
#10891=CARTESIAN_POINT ( 'NONE',  ( -3.081487911019577365E-30, 3.469446951953614189E-15, -4.900000000000015454 ) ) ;
#10899=DIRECTION ( 'NONE',  ( 0.000000000000000000, -8.482162385747133845E-47, 1.000000000000000000 ) ) ;
#10900=CARTESIAN_POINT ( 'NONE',  ( 5.000000000000001776, 1.953108124182678207, -0.2699991669428366547 ) ) ;
#10903=SURFACE_STYLE_USAGE ( .BOTH. , #12985 ) ;
#10926=CARTESIAN_POINT ( 'NONE',  ( -4.166666666666666963, 3.367876570272815950, -4.118275046351177693 ) ) ;
#10931=VERTEX_POINT ( 'NONE', #7444 ) ;
#10941=CARTESIAN_POINT ( 'NONE',  ( -5.170224855064538438, 2.788471980053851773, -4.589066185948671439 ) ) ;
#10975=FILL_AREA_STYLE ('',( #4131 ) ) ;
#10979=CARTESIAN_POINT ( 'NONE',  ( -0.2117491801717982791, -5.895756138069165431, -4.327903350935056181 ) ) ;
#10996=ORIENTED_EDGE ( 'NONE', *, *, #13383, .T. ) ;
#11000=ORIENTED_EDGE ( 'NONE', *, *, #4631, .T. ) ;
#11025=AXIS2_PLACEMENT_3D ( 'NONE', #167, #6524, #5441 ) ;
#11041=CIRCLE ( 'NONE', #1701, 6.532899837730830939 ) ;
#11048=SURFACE_STYLE_FILL_AREA ( #1092 ) ;
#11081=CARTESIAN_POINT ( 'NONE',  ( -5.000000000000000000, 2.886751345948124214, -4.284345921091780696 ) ) ;
#11091=ORIENTED_EDGE ( 'NONE', *, *, #206, .F. ) ;
#11093=CARTESIAN_POINT ( 'NONE',  ( -1.532072935877364915E-15, -6.066067634115591467, -4.659491423763650886 ) ) ;
#11094=ORIENTED_EDGE ( 'NONE', *, *, #499, .T. ) ;
#11105=ADVANCED_FACE ( 'NONE', ( #9287, #5977 ), #2484, .F. ) ;
#11109=ORIENTED_EDGE ( 'NONE', *, *, #13950, .F. ) ;
#11119=CARTESIAN_POINT ( 'NONE',  ( -5.000000000000000888, 2.424500739214329403, -0.4207179063848094369 ) ) ;
#11120=CARTESIAN_POINT ( 'NONE',  ( 5.000000000000000888, 0.000000000000000000, 0.000000000000000000 ) ) ;
#11151=DIRECTION ( 'NONE',  ( -1.000000000000000000, 0.000000000000000000, 0.000000000000000000 ) ) ;
#11154=CARTESIAN_POINT ( 'NONE',  ( -3.417629563437020401, 3.800333343455476687, -4.019399823475544586 ) ) ;
#11168=CARTESIAN_POINT ( 'NONE',  ( 5.000000000000001776, 2.886751345948152192, -0.5999999999999894307 ) ) ;
#11185=CARTESIAN_POINT ( 'NONE',  ( -5.000000000000000000, 2.886751345948124214, -0.5999999999999894307 ) ) ;
#11186=FACE_OUTER_BOUND ( 'NONE', #2461, .T. ) ;
#11198=ORIENTED_EDGE ( 'NONE', *, *, #5819, .F. ) ;
#11220=CARTESIAN_POINT ( 'NONE',  ( -4.817183509279845843, -3.279805190042321517, -4.566911319714218820 ) ) ;
#11236=ORIENTED_EDGE ( 'NONE', *, *, #1307, .F. ) ;
#11237=VERTEX_POINT ( 'NONE', #14136 ) ;
#11238=CIRCLE ( 'NONE', #8863, 0.5671001622691687061 ) ;
#11245=EDGE_CURVE ( 'NONE', #8967, #7349, #5400, .T. ) ;
#11246=CARTESIAN_POINT ( 'NONE',  ( 5.236973757159531395, -1.063254885194027333, -4.359289623603279651 ) ) ;
#11319=FACE_OUTER_BOUND ( 'NONE', #5419, .T. ) ;
#11333=CARTESIAN_POINT ( 'NONE',  ( 5.000000000000001776, 2.886751345948120662, -4.284345921091780696 ) ) ;
#11346=B_SPLINE_CURVE_WITH_KNOTS ( 'NONE', 3,
 ( #9702, #8589, #13077, #4303, #6396, #2014 ),
 .UNSPECIFIED., .F., .F.,
 ( 4, 2, 4 ),
 ( 0.000000000000000000, 0.0002514304509865737929, 0.0005028609019731475858 ),
 .UNSPECIFIED. ) ;
#11353=CARTESIAN_POINT ( 'NONE',  ( 2.500000000000000444, 3.469446951953614189E-15, -6.000000000000005329 ) ) ;
#11372=VERTEX_POINT ( 'NONE', #5473 ) ;
#11382=CARTESIAN_POINT ( 'NONE',  ( 5.244723105119098783, 2.047144756275687705, -4.475729968417853755 ) ) ;
#11388=CARTESIAN_POINT ( 'NONE',  ( 2.069940739436584298, -4.578421848776007330, -2.075823643836113210E-14 ) ) ;
#11401=CARTESIAN_POINT ( 'NONE',  ( 5.185163620697179176, 2.993655612200650573, -4.630826434870604302 ) ) ;
#11411=ORIENTED_EDGE ( 'NONE', *, *, #11650, .T. ) ;
#11423=DIRECTION ( 'NONE',  ( 0.000000000000000000, -8.482162385747133845E-47, 1.000000000000000000 ) ) ;
#11457=EDGE_CURVE ( 'NONE', #7155, #3422, #3435, .T. ) ;
#11466=CONICAL_SURFACE ( 'NONE', #4248, 6.726859516510133474, 1.221730476396048148 ) ;
#11482=VECTOR ( 'NONE', #5073, 1000.000000000000227 ) ;
#11496=ADVANCED_BREP_SHAPE_REPRESENTATION ( '', ( #6910, #11025 ), #5842 ) ;
#11497=FACE_OUTER_BOUND ( 'NONE', #5349, .T. ) ;
#11509=CARTESIAN_POINT ( 'NONE',  ( -5.000000000000001776, -2.886751345948152192, -0.5999999999999894307 ) ) ;
#11525=ORIENTED_EDGE ( 'NONE', *, *, #9134, .F. ) ;
#11531=CIRCLE ( 'NONE', #4086, 3.000000000000000888 ) ;
#11538=CARTESIAN_POINT ( 'NONE',  ( 5.000000000000000888, -2.426004080355346648, -0.4213009713786307620 ) ) ;
#11541=CIRCLE ( 'NONE', #6160, 3.000000000000000888 ) ;
#11551=CARTESIAN_POINT ( 'NONE',  ( 5.029396762153813150, 2.903723574490930659, -4.451008977024209834 ) ) ;
#11569=ORIENTED_EDGE ( 'NONE', *, *, #4447, .F. ) ;
#11575=EDGE_LOOP ( 'NONE', ( #3058, #5238, #5947 ) ) ;
#11611=DIRECTION ( 'NONE',  ( 0.000000000000000000, -8.482162385747133845E-47, 1.000000000000000000 ) ) ;
#11618=ORIENTED_EDGE ( 'NONE', *, *, #9846, .T. ) ;
#11631=CIRCLE ( 'NONE', #7178, 5.000000000000000888 ) ;
#11641=ADVANCED_FACE ( 'NONE', ( #4956 ), #6315, .T. ) ;
#11650=EDGE_CURVE ( 'NONE', #6870, #13190, #3294, .T. ) ;
#11651=VECTOR ( 'NONE', #4384, 999.9999999999998863 ) ;
#11654=FACE_OUTER_BOUND ( 'NONE', #1019, .T. ) ;
#11655=EDGE_LOOP ( 'NONE', ( #7293, #8313, #6974, #724, #3910, #6601 ) ) ;
#11659=VERTEX_POINT ( 'NONE', #3203 ) ;
#11660=CARTESIAN_POINT ( 'NONE',  ( 3.417629563436334728, 3.800333343455863044, -4.019399823475544586 ) ) ;
#11688=EDGE_CURVE ( 'NONE', #1738, #981, #4259, .T. ) ;
#11693=ORIENTED_EDGE ( 'NONE', *, *, #3890, .T. ) ;
#11698=CONICAL_SURFACE ( 'NONE', #13579, 2.450000000000000622, 0.9599310885968804774 ) ;
#11713=EDGE_CURVE ( 'NONE', #6044, #6152, #248, .T. ) ;
#11724=ORIENTED_EDGE ( 'NONE', *, *, #10428, .F. ) ;
#11726=CARTESIAN_POINT ( 'NONE',  ( 0.1702248550645342196, -5.871782057790571940, -4.589066185948686538 ) ) ;
#11747=CIRCLE ( 'NONE', #14103, 3.000000000000000888 ) ;
#11749=DIRECTION ( 'NONE',  ( 1.000000000000000000, 0.000000000000000000, 0.000000000000000000 ) ) ;
#11756=ORIENTED_EDGE ( 'NONE', *, *, #10353, .F. ) ;
#11768=DIRECTION ( 'NONE',  ( -1.000000000000000000, 0.000000000000000000, 0.000000000000000000 ) ) ;
#11771=ADVANCED_FACE ( 'NONE', ( #5862 ), #12413, .F. ) ;
#11778=ORIENTED_EDGE ( 'NONE', *, *, #7208, .F. ) ;
#11802=CARTESIAN_POINT ( 'NONE',  ( 3.401922400370089417, -3.809401878280050724, -4.271474537231044089 ) ) ;
#11803=CARTESIAN_POINT ( 'NONE',  ( 0.03111943836866019192, -6.084399642271201891, -4.666192694417985010 ) ) ;
#11811=LINE ( 'NONE', #12752, #13489 ) ;
#11813=CARTESIAN_POINT ( 'NONE',  ( 2.500000000000003553, 4.330127018922198978, -3.920524600599840426 ) ) ;
#11820=ORIENTED_EDGE ( 'NONE', *, *, #9846, .F. ) ;
#11832=CARTESIAN_POINT ( 'NONE',  ( -1.738710530748201144, -5.045296470309997616, -4.385927688751861453 ) ) ;
#11834=ORIENTED_EDGE ( 'NONE', *, *, #12024, .F. ) ;
#11836=CARTESIAN_POINT ( 'NONE',  ( -0.8333333333333353687, -5.292377467571613536, -4.118275046351175028 ) ) ;
#11869=CIRCLE ( 'NONE', #1334, 6.532899837730830939 ) ;
#11870=CARTESIAN_POINT ( 'NONE',  ( 4.296971609537261649, -3.292644976429659476, -4.396693167837900873 ) ) ;
#11871=CONICAL_SURFACE ( 'NONE', #13053, 6.726859516510133474, 1.221730476396048148 ) ;
#11872=CARTESIAN_POINT ( 'NONE',  ( -0.6806757771993166006, -5.380514348699412253, -4.138711833383711181 ) ) ;
#11880=UNCERTAINTY_MEASURE_WITH_UNIT (LENGTH_MEASURE( 1.000000000000000082E-05 ), #814, 'distance_accuracy_value', 'NONE');
#11920=CARTESIAN_POINT ( 'NONE',  ( 2.500000000000018652, 4.330127018922186544, 0.000000000000000000 ) ) ;
#11943=B_SPLINE_CURVE_WITH_KNOTS ( 'NONE', 3,
 ( #12279, #13394, #5604, #4541, #1435, #3368 ),
 .UNSPECIFIED., .F., .F.,
 ( 4, 2, 4 ),
 ( 0.004308305454211633703, 0.005784651566377418952, 0.007260997678543204201 ),
 .UNSPECIFIED. ) ;
#11952=ORIENTED_EDGE ( 'NONE', *, *, #6182, .F. ) ;
#11958=FACE_OUTER_BOUND ( 'NONE', #8547, .T. ) ;
#11980=CARTESIAN_POINT ( 'NONE',  ( -6.532899837730830939, 4.281373044485382480E-15, -6.000000000000005329 ) ) ;
#11998=CARTESIAN_POINT ( 'NONE',  ( 5.253368672218637236, -3.033033817057797510, -4.659491423763650886 ) ) ;
#12019=( LENGTH_UNIT ( ) NAMED_UNIT ( * ) SI_UNIT ( .MILLI., .METRE. ) );
#12024=EDGE_CURVE ( 'NONE', #2625, #641, #3094, .T. ) ;
#12026=CARTESIAN_POINT ( 'NONE',  ( 4.468294295033107599E-15, 5.914763229585228821, -4.581769937709100127 ) ) ;
#12046=CARTESIAN_POINT ( 'NONE',  ( -1.532072935877364915E-15, -6.066067634115591467, -4.659491423763650886 ) ) ;
#12047=APPLICATION_CONTEXT ( 'automotive_design' ) ;
#12058=B_SPLINE_CURVE_WITH_KNOTS ( 'NONE', 3,
 ( #12193, #6692, #12270, #5458, #8887, #8818, #6543, #1068 ),
 .UNSPECIFIED., .F., .F.,
 ( 4, 2, 2, 4 ),
 ( 2.451332856810596242E-07, 0.001475502392055661437, 0.002213131021440651464, 0.002950759650825642358 ),
 .UNSPECIFIED. ) ;
#12066=CARTESIAN_POINT ( 'NONE',  ( 5.236872748402769062, -0.5081686017868801697, -4.357689166958461868 ) ) ;
#12080=CARTESIAN_POINT ( 'NONE',  ( 5.000000000000000888, 0.9888715124523294042, -0.07061148569344773140 ) ) ;
#12093=CARTESIAN_POINT ( 'NONE',  ( -5.122335214190880670, 2.957381614792602864, -4.581769937709093909 ) ) ;
#12142=DIRECTION ( 'NONE',  ( 1.000000000000000000, 0.000000000000000000, 0.000000000000000000 ) ) ;
#12149=CARTESIAN_POINT ( 'NONE',  ( -1.738521435313292063, 5.045405839192970809, -4.385926550512752264 ) ) ;
#12162=TOROIDAL_SURFACE ( 'NONE', #7939, 6.532899837730830939, 0.5671001622691684840 ) ;
#12168=AXIS2_PLACEMENT_3D ( 'NONE', #9114, #10373, #4673 ) ;
#12189=DIRECTION ( 'NONE',  ( 0.000000000000000000, -1.000000000000000000, -8.482162385747133845E-47 ) ) ;
#12193=CARTESIAN_POINT ( 'NONE',  ( -5.000000000000000000, 2.886751345948124214, -0.5999999999999894307 ) ) ;
#12206=VECTOR ( 'NONE', #7964, 999.9999999999998863 ) ;
#12217=ORIENTED_EDGE ( 'NONE', *, *, #6137, .T. ) ;
#12226=FILL_AREA_STYLE_COLOUR ( '', #13301 ) ;
#12227=CARTESIAN_POINT ( 'NONE',  ( -0.4318028594007581322, 5.811705888748987192, -4.566911319714218820 ) ) ;
#12233=FACE_OUTER_BOUND ( 'NONE', #7681, .T. ) ;
#12246=EDGE_CURVE ( 'NONE', #8446, #11659, #10616, .T. ) ;
#12248=EDGE_CURVE ( 'NONE', #6044, #11659, #446, .T. ) ;
#12268=VERTEX_POINT ( 'NONE', #735 ) ;
#12270=CARTESIAN_POINT ( 'NONE',  ( -4.191707736911188142, 3.353419101626346155, -0.2701150775513927460 ) ) ;
#12279=CARTESIAN_POINT ( 'NONE',  ( -5.000000000000001776, -2.886751345948152192, -0.5999999999999894307 ) ) ;
#12300=DIRECTION ( 'NONE',  ( 0.000000000000000000, -8.482162385747133845E-47, 1.000000000000000000 ) ) ;
#12318=B_SPLINE_CURVE_WITH_KNOTS ( 'NONE', 3,
 ( #4632, #5837, #6950, #309, #8114, #3747 ),
 .UNSPECIFIED., .F., .F.,
 ( 4, 2, 4 ),
 ( 0.000000000000000000, 0.0002514304509865763950, 0.0005028609019731527900 ),
 .UNSPECIFIED. ) ;
#12329=CARTESIAN_POINT ( 'NONE',  ( -5.000000000000000000, 2.886751345948127767, -6.000000000000005329 ) ) ;
#12333=DIRECTION ( 'NONE',  ( -1.000000000000000000, 0.000000000000000000, 0.000000000000000000 ) ) ;
#12358=CARTESIAN_POINT ( 'NONE',  ( 0.4022569922705621637, -5.541259509125479710, -0.4198507760575922454 ) ) ;
#12363=ORIENTED_EDGE ( 'NONE', *, *, #1307, .T. ) ;
#12366=ORIENTED_EDGE ( 'NONE', *, *, #12248, .F. ) ;
#12367=SURFACE_SIDE_STYLE ('',( #11048 ) ) ;
#12397=CARTESIAN_POINT ( 'NONE',  ( -2.500000000000000444, 3.775608651740452848E-15, -5.624496230895170257 ) ) ;
#12398=AXIS2_PLACEMENT_3D ( 'NONE', #1663, #6112, #10594 ) ;
#12413=CONICAL_SURFACE ( 'NONE', #5164, 2.450000000000000622, 0.9599310885968804774 ) ;
#12431=ORIENTED_EDGE ( 'NONE', *, *, #13715, .T. ) ;
#12447=DIRECTION ( 'NONE',  ( -0.000000000000000000, 8.482162385747133845E-47, -1.000000000000000000 ) ) ;
#12475=CARTESIAN_POINT ( 'NONE',  ( -0.8441225671354688487, 5.568793373801097957, -4.476900509771803982 ) ) ;
#12478=AXIS2_PLACEMENT_3D ( 'NONE', #12329, #4646, #2301 ) ;
#12482=CARTESIAN_POINT ( 'NONE',  ( 0.000000000000000000, 0.000000000000000000, 0.000000000000000000 ) ) ;
#12497=CARTESIAN_POINT ( 'NONE',  ( 0.8333333333333322601, -5.292377467571611760, -4.118275046351174140 ) ) ;
#12517=( BOUNDED_SURFACE ( )  B_SPLINE_SURFACE ( 3, 2, ( 
 ( #6721, #8989, #6933 ),
 ( #8100, #1166, #84 ),
 ( #1458, #1375, #13628 ),
 ( #4687, #8175, #4617 ),
 ( #5690, #8034, #5902 ),
 ( #10233, #13549, #10386 ) ),
 .UNSPECIFIED., .F., .F., .T. ) 
 B_SPLINE_SURFACE_WITH_KNOTS ( ( 4, 2, 4 ),
 ( 3, 3 ),
 ( 0.02462896261017847102, 0.02769666342207012522, 0.03076436423396178288 ),
 ( 0.000000000000000000, 1.000000000000000000 ),
 .UNSPECIFIED. ) 
 GEOMETRIC_REPRESENTATION_ITEM ( )  RATIONAL_B_SPLINE_SURFACE ( (
 ( 1.000000000000000000, 0.8047780983185548465, 1.000000000000000000),
 ( 1.000000000000000000, 0.8123789199823617801, 1.000000000000000000),
 ( 1.000000000000000000, 0.8190678250840702779, 1.000000000000000000),
 ( 1.000000000000000000, 0.8192345812593594401, 1.000000000000000000),
 ( 1.000000000000000000, 0.8126126716515976733, 1.000000000000000000),
 ( 1.000000000000000000, 0.8047712641343244266, 1.000000000000000000) ) ) 
 REPRESENTATION_ITEM ( '' )  SURFACE ( )  );
#12534=CARTESIAN_POINT ( 'NONE',  ( -0.7030283904642582460, 5.367609061415551608, -4.396693167835974414 ) ) ;
#12539=EDGE_CURVE ( 'NONE', #9023, #6870, #14377, .T. ) ;
#12543=ADVANCED_FACE ( 'NONE', ( #4675 ), #3587, .F. ) ;
#12545=DIRECTION ( 'NONE',  ( 0.000000000000000000, 8.482162385747133845E-47, -1.000000000000000000 ) ) ;
#12598=CARTESIAN_POINT ( 'NONE',  ( -2.500000000000016875, -4.330127018922186544, 0.000000000000000000 ) ) ;
#12604=DIRECTION ( 'NONE',  ( 0.000000000000000000, -8.482162385747133845E-47, 1.000000000000000000 ) ) ;
#12621=DIRECTION ( 'NONE',  ( 0.000000000000000000, -8.482162385747133845E-47, 1.000000000000000000 ) ) ;
#12656=ADVANCED_FACE ( 'NONE', ( #12233 ), #8781, .T. ) ;
#12669=CARTESIAN_POINT ( 'NONE',  ( -5.122335214190881558, -2.957381614792619740, -4.581769937709098350 ) ) ;
#12675=CARTESIAN_POINT ( 'NONE',  ( 5.253368672218638125, 3.033033817057769532, -4.659491423763650886 ) ) ;
#12680=CARTESIAN_POINT ( 'NONE',  ( 0.8441225671342533765, 5.568793373800017932, -4.476900509771413184 ) ) ;
#12705=CARTESIAN_POINT ( 'NONE',  ( -2.499999999999995115, -4.330127018922216742, -3.920524600599868403 ) ) ;
#12718=ADVANCED_FACE ( 'NONE', ( #5296 ), #7554, .F. ) ;
#12729=CLOSED_SHELL ( 'NONE', ( #867, #4874, #11771, #1355, #5751, #12718, #12543, #1086, #12656, #3159, #6539, #6357, #995, #11105, #8976, #8541, #9084, #8438, #2029, #2525, #1642, #2441, #11641, #12895, #7847, #1921, #2427, #9552, #2857, #10756, #6159, #10187 ) ) ;
#12732=EDGE_CURVE ( 'NONE', #2625, #981, #89, .T. ) ;
#12752=CARTESIAN_POINT ( 'NONE',  ( 3.370256023960729782E-15, 5.773502691896274186, -6.000000000000005329 ) ) ;
#12785=CARTESIAN_POINT ( 'NONE',  ( -1.642566673137935362, -4.825166380998194171, -0.07080520455422933956 ) ) ;
#12804=EDGE_CURVE ( 'NONE', #6152, #641, #1483, .T. ) ;
#12826=CARTESIAN_POINT ( 'NONE',  ( 0.2117491801717920341, -5.895756138069166319, -4.327903350935056181 ) ) ;
#12828=( BOUNDED_SURFACE ( )  B_SPLINE_SURFACE ( 3, 2, ( 
 ( #1778, #7166, #6067 ),
 ( #8420, #11870, #2887 ),
 ( #460, #11802, #8568 ),
 ( #6225, #5209, #8501 ),
 ( #13863, #10698, #2957 ),
 ( #7393, #1848, #10979 ) ),
 .UNSPECIFIED., .F., .F., .F. ) 
 B_SPLINE_SURFACE_WITH_KNOTS ( ( 4, 2, 4 ),
 ( 3, 3 ),
 ( 0.002450104044831693303, 0.005591829551853680358, 0.008733555058875666979 ),
 ( 0.000000000000000000, 1.000000000000000000 ),
 .UNSPECIFIED. ) 
 GEOMETRIC_REPRESENTATION_ITEM ( )  RATIONAL_B_SPLINE_SURFACE ( (
 ( 1.000000000000000000, 0.8047731410850403888, 1.000000000000000000),
 ( 1.000000000000000000, 0.8125552299157110525, 1.000000000000000000),
 ( 1.000000000000000000, 0.8191520442888694520, 1.000000000000000000),
 ( 1.000000000000000000, 0.8191520442891048193, 1.000000000000000000),
 ( 1.000000000000000000, 0.8125552299155338609, 1.000000000000000000),
 ( 1.000000000000000000, 0.8047731410850404998, 1.000000000000000000) ) ) 
 REPRESENTATION_ITEM ( '' )  SURFACE ( )  );
#12840=B_SPLINE_CURVE_WITH_KNOTS ( 'NONE', 3,
 ( #10781, #9686, #8574, #1712, #3112, #12993 ),
 .UNSPECIFIED., .F., .F.,
 ( 4, 2, 4 ),
 ( 0.000000000000000000, 0.001529397995383605015, 0.003058795990767210031 ),
 .UNSPECIFIED. ) ;
#12841=LINE ( 'NONE', #7265, #11482 ) ;
#12867=CARTESIAN_POINT ( 'NONE',  ( -2.285412292771025644, -4.454019289455653841, -1.712841791506071108E-14 ) ) ;
#12892=AXIS2_PLACEMENT_3D ( 'NONE', #8678, #8817, #7859 ) ;
#12893=ORIENTED_EDGE ( 'NONE', *, *, #13005, .F. ) ;
#12895=ADVANCED_FACE ( 'NONE', ( #11497 ), #14331, .F. ) ;
#12905=CARTESIAN_POINT ( 'NONE',  ( -3.417629563435960804, -3.800333343456104185, -4.019399823475084510 ) ) ;
#12911=EDGE_LOOP ( 'NONE', ( #12363, #7560, #12893, #11569 ) ) ;
#12920=CARTESIAN_POINT ( 'NONE',  ( -5.248984340851197139, -2.531668808681911909, -4.566868479993924090 ) ) ;
#12957=EDGE_LOOP ( 'NONE', ( #8073, #5225, #9099 ) ) ;
#12963=ORIENTED_EDGE ( 'NONE', *, *, #7052, .F. ) ;
#12964=EDGE_CURVE ( 'NONE', #13190, #4994, #7291, .T. ) ;
#12978=CARTESIAN_POINT ( 'NONE',  ( 1.738710530748207583, 5.045296470309983405, -4.385927688751852571 ) ) ;
#12985=SURFACE_SIDE_STYLE ('',( #2134 ) ) ;
#12993=CARTESIAN_POINT ( 'NONE',  ( 5.236872748402767286, 8.765285303662936917E-14, -4.357689166958464533 ) ) ;
#13005=EDGE_CURVE ( 'NONE', #6697, #7073, #4921, .T. ) ;
#13007=DIRECTION ( 'NONE',  ( 0.000000000000000000, -8.482162385747133845E-47, 1.000000000000000000 ) ) ;
#13010=B_SPLINE_CURVE_WITH_KNOTS ( 'NONE', 3,
 ( #11333, #3663, #11551, #364, #11401, #9282 ),
 .UNSPECIFIED., .F., .F.,
 ( 4, 2, 4 ),
 ( 0.000000000000000000, 0.0002514304509865741182, 0.0005028609019731482364 ),
 .UNSPECIFIED. ) ;
#13012=VERTEX_POINT ( 'NONE', #14367 ) ;
#13019=EDGE_CURVE ( 'NONE', #8446, #7155, #11747, .T. ) ;
#13024=CARTESIAN_POINT ( 'NONE',  ( 4.191707736911188142, -3.353419101626373244, -0.2701150775514071789 ) ) ;
#13053=AXIS2_PLACEMENT_3D ( 'NONE', #1080, #5536, #9791 ) ;
#13065=VECTOR ( 'NONE', #1137, 1000.000000000000227 ) ;
#13077=CARTESIAN_POINT ( 'NONE',  ( 5.029396762153807821, -2.903723574490948423, -4.451008977024202729 ) ) ;
#13080=ORIENTED_EDGE ( 'NONE', *, *, #8136, .T. ) ;
#13092=CARTESIAN_POINT ( 'NONE',  ( 5.253368672218637236, -3.033033817057797510, -4.659491423763650886 ) ) ;
#13105=CARTESIAN_POINT ( 'NONE',  ( 5.238715782502664453, -1.018209582082216347, -4.386015505371676504 ) ) ;
#13133=CARTESIAN_POINT ( 'NONE',  ( 3.332577314687724973E-15, 5.773502691896274186, -4.369520038198757561 ) ) ;
#13147=ORIENTED_EDGE ( 'NONE', *, *, #11457, .F. ) ;
#13158=CARTESIAN_POINT ( 'NONE',  ( -2.069940739436577193, 4.578421848775986014, -3.163668057994810583E-15 ) ) ;
#13169=B_SPLINE_CURVE_WITH_KNOTS ( 'NONE', 3,
 ( #1866, #10791, #6090, #559, #5015, #13946, #3997, #772 ),
 .UNSPECIFIED., .F., .F.,
 ( 4, 2, 2, 4 ),
 ( 2.451332856815838846E-07, 0.001475502392055680735, 0.002213131021440680520, 0.002950759650825679654 ),
 .UNSPECIFIED. ) ;
#13178=CARTESIAN_POINT ( 'NONE',  ( -2.500000000000011990, 4.330127018922186544, 0.000000000000000000 ) ) ;
#13190=VERTEX_POINT ( 'NONE', #9140 ) ;
#13192=VERTEX_POINT ( 'NONE', #6944 ) ;
#13193=CARTESIAN_POINT ( 'NONE',  ( -4.378301941662546604, 3.528365556573288320, -4.490643565754954381 ) ) ;
#13200=ORIENTED_EDGE ( 'NONE', *, *, #7390, .T. ) ;
#13223=CARTESIAN_POINT ( 'NONE',  ( -3.081487911019577365E-30, 3.469446951953614189E-15, -25.03750572909319061 ) ) ;
#13226=CARTESIAN_POINT ( 'NONE',  ( 6.532899837730830939, 3.469446951953614189E-15, -5.432899837730820636 ) ) ;
#13232=CARTESIAN_POINT ( 'NONE',  ( 2.450000000000000622, 0.000000000000000000, -0.3851141460153306717 ) ) ;
#13236=ORIENTED_EDGE ( 'NONE', *, *, #11457, .T. ) ;
#13251=EDGE_LOOP ( 'NONE', ( #13502, #8677, #12963 ) ) ;
#13254=CARTESIAN_POINT ( 'NONE',  ( -5.000000000000000000, 0.4965892259340516923, -0.01450341304856382109 ) ) ;
#13289=EDGE_CURVE ( 'NONE', #4994, #10243, #62, .T. ) ;
#13301=COLOUR_RGB ( '', 0.09019608, 0.27058824, 0.51372549) ;
#13336=CARTESIAN_POINT ( 'NONE',  ( 5.000000000000001776, 2.886751345948127767, -6.000000000000005329 ) ) ;
#13339=ORIENTED_EDGE ( 'NONE', *, *, #1776, .T. ) ;
#13358=ORIENTED_EDGE ( 'NONE', *, *, #2358, .F. ) ;
#13383=EDGE_CURVE ( 'NONE', #6697, #1128, #2848, .T. ) ;
#13394=CARTESIAN_POINT ( 'NONE',  ( -4.999999999999999112, -2.426004080355347980, -0.4213009713786298738 ) ) ;
#13397=LINE ( 'NONE', #10828, #6718 ) ;
#13425=CARTESIAN_POINT ( 'NONE',  ( -2.068360682592150557, -4.579334095020470841, -0.01465562841809295996 ) ) ;
#13434=PLANE ( 'NONE',  #4457 ) ;
#13442=CARTESIAN_POINT ( 'NONE',  ( -1.647413659512543482, 4.822367972110034096, -0.05822226285683312907 ) ) ;
#13445=CARTESIAN_POINT ( 'NONE',  ( -2.500000000000016875, -4.330127018922186544, 0.000000000000000000 ) ) ;
#13457=CARTESIAN_POINT ( 'NONE',  ( -3.081487911019577365E-30, 3.469446951953614189E-15, -5.974599999999997024 ) ) ;
#13466=LINE ( 'NONE', #3436, #5617 ) ;
#13471=ORIENTED_EDGE ( 'NONE', *, *, #9598, .T. ) ;
#13475=CARTESIAN_POINT ( 'NONE',  ( 4.817220356105922363, -3.279784343982821593, -4.566919140436432656 ) ) ;
#13476=CARTESIAN_POINT ( 'NONE',  ( -3.081487911019577365E-30, 3.469446951953614189E-15, -6.000000000000005329 ) ) ;
#13489=VECTOR ( 'NONE', #10638, 1000.000000000000000 ) ;
#13502=ORIENTED_EDGE ( 'NONE', *, *, #4516, .F. ) ;
#13504=ORIENTED_EDGE ( 'NONE', *, *, #5664, .T. ) ;
#13528=CARTESIAN_POINT ( 'NONE',  ( 5.000000000000001776, 3.083561708551495695, -4.589114193688893728 ) ) ;
#13529=EDGE_CURVE ( 'NONE', #3422, #11659, #4067, .T. ) ;
#13544=ORIENTED_EDGE ( 'NONE', *, *, #6182, .T. ) ;
#13549=CARTESIAN_POINT ( 'NONE',  ( -5.000000000000000000, -3.083558758346089945, -4.589113630813312028 ) ) ;
#13560=AXIS2_PLACEMENT_3D ( 'NONE', #2709, #6130, #3813 ) ;
#13579=AXIS2_PLACEMENT_3D ( 'NONE', #3387, #12300, #9806 ) ;
#13606=CARTESIAN_POINT ( 'NONE',  ( 5.236773790937433226, 1.020504364866074987, -4.356121212116739194 ) ) ;
#13610=MECHANICAL_DESIGN_GEOMETRIC_PRESENTATION_REPRESENTATION('',(#2372),#8681);
#13628=CARTESIAN_POINT ( 'NONE',  ( -5.236972091263603524, 1.063041182845755772, -4.359263227153169495 ) ) ;
#13661=CARTESIAN_POINT ( 'NONE',  ( -2.930059260563458778, -4.081832189068413719, -1.671478349248484320E-14 ) ) ;
#13682=CARTESIAN_POINT ( 'NONE',  ( 5.000000000000001776, -1.088253076326978874, -4.021000279465625660 ) ) ;
#13686=B_SPLINE_CURVE_WITH_KNOTS ( 'NONE', 3,
 ( #14121, #8470, #13024, #5099, #10671, #3000, #7431, #13968 ),
 .UNSPECIFIED., .F., .F.,
 ( 4, 2, 2, 4 ),
 ( 2.451332856810592536E-07, 0.001475502392055651462, 0.002213131021440637152, 0.002950759650825622842 ),
 .UNSPECIFIED. ) ;
#13703=B_SPLINE_CURVE_WITH_KNOTS ( 'NONE', 3,
 ( #14424, #8776, #13254, #83, #3231, #4484, #11119, #11185 ),
 .UNSPECIFIED., .F., .F.,
 ( 4, 2, 2, 4 ),
 ( 0.007260997678543204201, 0.007995810154593245220, 0.008730622630643287974, 0.01020024758274337001 ),
 .UNSPECIFIED. ) ;
#13709=CARTESIAN_POINT ( 'NONE',  ( 0.000000000000000000, 0.000000000000000000, 0.000000000000000000 ) ) ;
#13715=EDGE_CURVE ( 'NONE', #3061, #8941, #11346, .T. ) ;
#13717=ORIENTED_EDGE ( 'NONE', *, *, #12804, .F. ) ;
#13728=CARTESIAN_POINT ( 'NONE',  ( -5.000000000000000000, 2.886751345948124214, -4.284345921091780696 ) ) ;
#13745=DIRECTION ( 'NONE',  ( 0.000000000000000000, -8.482162385747133845E-47, 1.000000000000000000 ) ) ;
#13751=CARTESIAN_POINT ( 'NONE',  ( 4.166666666666667851, -3.367876570272840819, -4.118275046351178581 ) ) ;
#13769=CARTESIAN_POINT ( 'NONE',  ( 2.602085213965210642E-15, 5.773502691896270633, 0.000000000000000000 ) ) ;
#13815=VECTOR ( 'NONE', #4544, 1000.000000000000000 ) ;
#13822=FACE_OUTER_BOUND ( 'NONE', #6677, .T. ) ;
#13828=CARTESIAN_POINT ( 'NONE',  ( -1.752700365193367750E-15, -5.773502691896304384, -4.284345921091780696 ) ) ;
#13863=CARTESIAN_POINT ( 'NONE',  ( 0.8441225671340620851, -5.568793373800590807, -4.476900509771624570 ) ) ;
#13895=DIRECTION ( 'NONE',  ( 0.000000000000000000, 8.482162385747133845E-47, -1.000000000000000000 ) ) ;
#13912=FACE_OUTER_BOUND ( 'NONE', #9270, .T. ) ;
#13920=DIRECTION ( 'NONE',  ( 0.000000000000000000, -8.482162385747133845E-47, 1.000000000000000000 ) ) ;
#13929=CARTESIAN_POINT ( 'NONE',  ( -4.296971609537496128, -3.292644976429660808, -4.396693167836204452 ) ) ;
#13941=ORIENTED_EDGE ( 'NONE', *, *, #13383, .F. ) ;
#13944=EDGE_LOOP ( 'NONE', ( #9199, #9614 ) ) ;
#13946=CARTESIAN_POINT ( 'NONE',  ( 2.068360682592138122, 4.579334095020464623, -0.01465562841808510514 ) ) ;
#13950=EDGE_CURVE ( 'NONE', #11237, #14260, #8735, .T. ) ;
#13968=CARTESIAN_POINT ( 'NONE',  ( 2.500000000000011546, -4.330127018922186544, 0.000000000000000000 ) ) ;
#13969=CONICAL_SURFACE ( 'NONE', #865, 5.000000000000000888, 0.9110539511682884672 ) ;
#13971=AXIS2_PLACEMENT_3D ( 'NONE', #64, #7806, #6701 ) ;
#13986=CYLINDRICAL_SURFACE ( 'NONE', #4728, 3.000000000000000888 ) ;
#13987=B_SPLINE_CURVE_WITH_KNOTS ( 'NONE', 3,
 ( #13728, #1345, #7043, #1498, #6844 ),
 .UNSPECIFIED., .F., .F.,
 ( 4, 1, 4 ),
 ( 0.000000000000000000, 0.002886751345948135056, 0.005773502691896270113 ),
 .UNSPECIFIED. ) ;
#13992=CARTESIAN_POINT ( 'NONE',  ( 3.500188911486806997, 4.028306647601582746, -4.385926550512752264 ) ) ;
#13994=ORIENTED_EDGE ( 'NONE', *, *, #4200, .F. ) ;
#13999=ORIENTED_EDGE ( 'NONE', *, *, #13529, .T. ) ;
#14006=STYLED_ITEM ( 'NONE', ( #3305 ), #6910 ) ;
#14015=DIRECTION ( 'NONE',  ( -0.8660254037844372643, -0.5000000000000023315, -2.348866325434636703E-33 ) ) ;
#14044=CIRCLE ( 'NONE', #14273, 2.500000000000000444 ) ;
#14045=CARTESIAN_POINT ( 'NONE',  ( -4.166666666666669627, -3.367876570272843928, -4.118275046351176805 ) ) ;
#14067=FACE_OUTER_BOUND ( 'NONE', #9177, .T. ) ;
#14080=VECTOR ( 'NONE', #11423, 1000.000000000000000 ) ;
#14103=AXIS2_PLACEMENT_3D ( 'NONE', #4498, #1254, #2061 ) ;
#14105=CARTESIAN_POINT ( 'NONE',  ( -3.081487911019577365E-30, 3.469446951953614189E-15, -6.000000000000005329 ) ) ;
#14112=DIRECTION ( 'NONE',  ( 0.000000000000000000, -8.482162385747133845E-47, 1.000000000000000000 ) ) ;
#14121=CARTESIAN_POINT ( 'NONE',  ( 5.000000000000000000, -2.886751345948152192, -0.5999999999999894307 ) ) ;
#14136=CARTESIAN_POINT ( 'NONE',  ( -5.253368672218639013, -3.033033817057793957, -4.659491423763650886 ) ) ;
#14158=PLANE ( 'NONE',  #7853 ) ;
#14203=CARTESIAN_POINT ( 'NONE',  ( -3.081487911019577365E-30, 3.469446951953614189E-15, -25.03750572909319061 ) ) ;
#14207=ORIENTED_EDGE ( 'NONE', *, *, #13019, .F. ) ;
#14221=CONICAL_SURFACE ( 'NONE', #5772, 3.000000000000000888, 0.9599310885968798113 ) ;
#14223=CARTESIAN_POINT ( 'NONE',  ( 3.667453972563985829E-15, 6.066067634115573703, -4.659491423763650886 ) ) ;
#14253=CARTESIAN_POINT ( 'NONE',  ( -3.081487911019577365E-30, 3.469446951953614189E-15, -5.624496230895170257 ) ) ;
#14260=VERTEX_POINT ( 'NONE', #9894 ) ;
#14273=AXIS2_PLACEMENT_3D ( 'NONE', #8973, #6773, #6554 ) ;
#14301=DIRECTION ( 'NONE',  ( -0.5000000000000033307, -0.8660254037844368202, 8.404057939144363410E-32 ) ) ;
#14325=CARTESIAN_POINT ( 'NONE',  ( -4.319324222799853175, 3.279739689145492854, -4.138711833384279615 ) ) ;
#14331=( BOUNDED_SURFACE ( )  B_SPLINE_SURFACE ( 3, 2, ( 
 ( #3838, #8270, #7538 ),
 ( #4135, #13929, #6376 ),
 ( #12905, #686, #8502 ),
 ( #7328, #7246, #3902 ),
 ( #11872, #10700, #2888 ),
 ( #12826, #11726, #11803 ) ),
 .UNSPECIFIED., .F., .F., .T. ) 
 B_SPLINE_SURFACE_WITH_KNOTS ( ( 4, 2, 4 ),
 ( 3, 3 ),
 ( 0.002450104044831692002, 0.005591829551853677756, 0.008733555058875663510 ),
 ( 0.000000000000000000, 1.000000000000000000 ),
 .UNSPECIFIED. ) 
 GEOMETRIC_REPRESENTATION_ITEM ( )  RATIONAL_B_SPLINE_SURFACE ( (
 ( 1.000000000000000000, 0.8047731410850404998, 1.000000000000000000),
 ( 1.000000000000000000, 0.8125552299158004255, 1.000000000000000000),
 ( 1.000000000000000000, 0.8191520442887517683, 1.000000000000000000),
 ( 1.000000000000000000, 0.8191520442892222809, 1.000000000000000000),
 ( 1.000000000000000000, 0.8125552299154461533, 1.000000000000000000),
 ( 1.000000000000000000, 0.8047731410850398337, 1.000000000000000000) ) ) 
 REPRESENTATION_ITEM ( '' )  SURFACE ( )  );
#14367=CARTESIAN_POINT ( 'NONE',  ( -1.752700365193367750E-15, -5.773502691896304384, -4.284345921091780696 ) ) ;
#14369=EDGE_LOOP ( 'NONE', ( #567, #6758, #289, #9123 ) ) ;
#14375=DIRECTION ( 'NONE',  ( 0.8660254037844367092, -0.5000000000000032196, 2.348866325434811866E-33 ) ) ;
#14377=B_SPLINE_CURVE_WITH_KNOTS ( 'NONE', 3,
 ( #2550, #11538, #6039, #282, #4748, #9195 ),
 .UNSPECIFIED., .F., .F.,
 ( 4, 2, 4 ),
 ( 0.004308305454211655387, 0.005784651566377436299, 0.007260997678543217211 ),
 .UNSPECIFIED. ) ;
#14382=CARTESIAN_POINT ( 'NONE',  ( 5.000000000000000000, -2.886751345948148639, -4.284345921091780696 ) ) ;
#14390=CARTESIAN_POINT ( 'NONE',  ( -3.500188911486803889, -4.028306647601596069, -4.385926550512758482 ) ) ;
#14395=CARTESIAN_POINT ( 'NONE',  ( -3.401922400371467425, 3.809401878279565334, -4.271474537231044977 ) ) ;
#14397=DIRECTION ( 'NONE',  ( -1.000000000000000000, 0.000000000000000000, 0.000000000000000000 ) ) ;
#14411=FACE_OUTER_BOUND ( 'NONE', #13944, .T. ) ;
#14424=CARTESIAN_POINT ( 'NONE',  ( -5.000000000000000888, 0.000000000000000000, 0.000000000000000000 ) ) ;
#14464=ORIENTED_EDGE ( 'NONE', *, *, #5819, .T. ) ;
ENDSEC;
END-ISO-10303-21;
